ISO-10303-21;
HEADER;
FILE_DESCRIPTION (('STEP AP214'),
    '1' );
FILE_NAME ('radial cylindrical roller bearing_iso_ISO 15 RCR - 1712 - 24,SI,NC,24.step',
    '2026-10-08T13:46:47',
    ( '' ),
    ( '' ),
    'SwSTEP 2.0',
    'SolidWorks 2026',
    '' );
FILE_SCHEMA (( 'AUTOMOTIVE_DESIGN' ));
ENDSEC;

DATA;
#4=CIRCLE ( 'NONE', #19877, 8.800000000000023803 ) ;
#12=DIRECTION ( 'NONE',  ( 1.000000000000000000, 0.000000000000000000, 0.000000000000000000 ) ) ;
#37=CIRCLE ( 'NONE', #17650, 6.543750000000021494 ) ;
#78=ORIENTED_EDGE ( 'NONE', *, *, #18290, .F. ) ;
#145=DIRECTION ( 'NONE',  ( 1.000000000000000000, 0.000000000000000000, 0.000000000000000000 ) ) ;
#160=SHAPE_REPRESENTATION_RELATIONSHIP ( 'NONE' , 'NONE' ,  #21657, #23316 ) ;
#178=AXIS2_PLACEMENT_3D ( 'NONE', #2507, #15364, #6234 ) ;
#199=CARTESIAN_POINT ( 'NONE',  ( -2.000000000000001776, 8.130889342088984924E-16, 6.543750000000021494 ) ) ;
#209=ORIENTED_EDGE ( 'NONE', *, *, #10563, .F. ) ;
#217=DIRECTION ( 'NONE',  ( 1.000000000000000000, 0.000000000000000000, 0.000000000000000000 ) ) ;
#228=DIRECTION ( 'NONE',  ( 0.000000000000000000, 0.000000000000000000, -1.000000000000000000 ) ) ;
#302=EDGE_CURVE ( 'NONE', #23443, #22486, #15470, .T. ) ;
#341=DIRECTION ( 'NONE',  ( 1.000000000000000000, 0.000000000000000000, 0.000000000000000000 ) ) ;
#358=CARTESIAN_POINT ( 'NONE',  ( -90.00000000000000000, 0.000000000000000000, 0.000000000000000000 ) ) ;
#364=AXIS2_PLACEMENT_3D ( 'NONE', #4231, #22417, #9754 ) ;
#401=CARTESIAN_POINT ( 'NONE',  ( 1.519999999999999574, 0.000000000000000000, -6.760799999999997034 ) ) ;
#410=DIRECTION ( 'NONE',  ( -1.000000000000000000, 0.000000000000000000, -0.000000000000000000 ) ) ;
#412=ORIENTED_EDGE ( 'NONE', *, *, #302, .T. ) ;
#480=CIRCLE ( 'NONE', #8921, 0.03079999999999836341 ) ;
#484=EDGE_CURVE ( 'NONE', #12003, #2520, #19247, .T. ) ;
#498=ORIENTED_EDGE ( 'NONE', *, *, #23535, .T. ) ;
#520=PRODUCT_DEFINITION ( 'UNKNOWN', '', #22130, #7875 ) ;
#521=AXIS2_PLACEMENT_3D ( 'NONE', #5030, #23463, #14389 ) ;
#539=ORIENTED_EDGE ( 'NONE', *, *, #10100, .T. ) ;
#566=CARTESIAN_POINT ( 'NONE',  ( 1.600000000000004086, 8.247996192257451316E-16, 6.735000000000022524 ) ) ;
#570=ORIENTED_EDGE ( 'NONE', *, *, #15740, .T. ) ;
#572=DIRECTION ( 'NONE',  ( 0.000000000000000000, 0.000000000000000000, -1.000000000000000000 ) ) ;
#578=CARTESIAN_POINT ( 'NONE',  ( -1.600000000000004086, 1.012170579495290078E-15, 8.265000000000021885 ) ) ;
#581=DIRECTION ( 'NONE',  ( 0.000000000000000000, 0.000000000000000000, -1.000000000000000000 ) ) ;
#623=CARTESIAN_POINT ( 'NONE',  ( 2.000000000000001776, 0.000000000000000000, 0.000000000000000000 ) ) ;
#643=CARTESIAN_POINT ( 'NONE',  ( 1.506022603841227436, 0.000000000000000000, 0.000000000000000000 ) ) ;
#700=AXIS2_PLACEMENT_3D ( 'NONE', #22724, #17242, #13777 ) ;
#701=VERTEX_POINT ( 'NONE', #9115 ) ;
#703=CARTESIAN_POINT ( 'NONE',  ( -1.800000000000000711, 0.000000000000000000, 0.000000000000000000 ) ) ;
#718=CYLINDRICAL_SURFACE ( 'NONE', #10195, 6.735000000000022524 ) ;
#816=ORIENTED_EDGE ( 'NONE', *, *, #15740, .F. ) ;
#846=EDGE_CURVE ( 'NONE', #18380, #19075, #883, .T. ) ;
#861=EDGE_LOOP ( 'NONE', ( #16824, #10208, #1219, #4381 ) ) ;
#873=DIRECTION ( 'NONE',  ( -0.000000000000000000, -1.000000000000000000, -0.000000000000000000 ) ) ;
#883=CIRCLE ( 'NONE', #20760, 6.760799999999997034 ) ;
#892=VERTEX_POINT ( 'NONE', #11261 ) ;
#899=CLOSED_SHELL ( 'NONE', ( #6786, #11905, #3624, #2468, #18257, #22732, #4967, #5923, #20896, #22223, #13537, #1331, #3504, #3622, #20645, #21658, #19766, #6994, #8913, #3077, #23572, #6544, #2801, #1115, #10733, #19579, #15407, #6610, #17618, #7501, #9069, #8508, #2462, #21902, #20125, #19166, #8329, #3031, #5399, #13635, #21038, #15573, #18663, #22672 ) ) ;
#901=ORIENTED_EDGE ( 'NONE', *, *, #10609, .F. ) ;
#987=ORIENTED_EDGE ( 'NONE', *, *, #1335, .T. ) ;
#991=DIRECTION ( 'NONE',  ( 1.000000000000000000, 0.000000000000000000, 0.000000000000000000 ) ) ;
#999=CARTESIAN_POINT ( 'NONE',  ( 1.600000000000004086, 0.000000000000000000, 0.000000000000000000 ) ) ;
#1018=ORIENTED_EDGE ( 'NONE', *, *, #12945, .T. ) ;
#1036=DIRECTION ( 'NONE',  ( 0.000000000000000000, 0.000000000000000000, -1.000000000000000000 ) ) ;
#1069=ORIENTED_EDGE ( 'NONE', *, *, #20166, .F. ) ;
#1070=AXIS2_PLACEMENT_3D ( 'NONE', #18321, #15001, #13305 ) ;
#1078=CIRCLE ( 'NONE', #21277, 0.03079999999999923077 ) ;
#1115=ADVANCED_FACE ( 'NONE', ( #10855 ), #15882, .T. ) ;
#1137=CIRCLE ( 'NONE', #23336, 9.000000000000021316 ) ;
#1163=DIRECTION ( 'NONE',  ( 1.000000000000000000, 0.000000000000000000, 0.000000000000000000 ) ) ;
#1190=FACE_BOUND ( 'NONE', #7353, .T. ) ;
#1219=ORIENTED_EDGE ( 'NONE', *, *, #17180, .F. ) ;
#1272=EDGE_CURVE ( 'NONE', #22486, #7327, #22825, .T. ) ;
#1276=ORIENTED_EDGE ( 'NONE', *, *, #7465, .F. ) ;
#1289=CARTESIAN_POINT ( 'NONE',  ( -90.00000000000000000, 0.000000000000000000, -8.073750000000021743 ) ) ;
#1304=DIRECTION ( 'NONE',  ( 1.000000000000000000, -0.000000000000000000, -0.000000000000000000 ) ) ;
#1322=CARTESIAN_POINT ( 'NONE',  ( -1.489200000000000079, 8.279592079675421725E-16, 6.760799999999997034 ) ) ;
#1331=ADVANCED_FACE ( 'NONE', ( #7254 ), #1950, .F. ) ;
#1335=EDGE_CURVE ( 'NONE', #10183, #22486, #22181, .T. ) ;
#1336=AXIS2_PLACEMENT_3D ( 'NONE', #19570, #6898, #21593 ) ;
#1368=ORIENTED_EDGE ( 'NONE', *, *, #10563, .T. ) ;
#1374=CARTESIAN_POINT ( 'NONE',  ( 1.799999999999996048, 1.102182119232620869E-15, 9.000000000000023093 ) ) ;
#1385=LINE ( 'NONE', #3315, #2950 ) ;
#1393=EDGE_CURVE ( 'NONE', #22332, #19018, #22039, .T. ) ;
#1398=AXIS2_PLACEMENT_3D ( 'NONE', #703, #8039, #228 ) ;
#1408=ORIENTED_EDGE ( 'NONE', *, *, #14798, .F. ) ;
#1415=FACE_OUTER_BOUND ( 'NONE', #16177, .T. ) ;
#1416=ORIENTED_EDGE ( 'NONE', *, *, #16738, .F. ) ;
#1434=EDGE_CURVE ( 'NONE', #2153, #12123, #14043, .T. ) ;
#1453=ORIENTED_EDGE ( 'NONE', *, *, #3608, .F. ) ;
#1476=CARTESIAN_POINT ( 'NONE',  ( 2.000000000000001776, 0.000000000000000000, 0.000000000000000000 ) ) ;
#1479=CARTESIAN_POINT ( 'NONE',  ( -90.00000000000000000, 0.000000000000000000, 0.000000000000000000 ) ) ;
#1488=EDGE_LOOP ( 'NONE', ( #20968, #10757, #16555, #15110 ) ) ;
#1515=FACE_OUTER_BOUND ( 'NONE', #19754, .T. ) ;
#1538=ORIENTED_EDGE ( 'NONE', *, *, #1994, .F. ) ;
#1554=CIRCLE ( 'NONE', #3866, 0.1999999999999996503 ) ;
#1628=DIRECTION ( 'NONE',  ( 1.000000000000000000, -0.000000000000000000, -0.000000000000000000 ) ) ;
#1637=EDGE_LOOP ( 'NONE', ( #4447, #2835 ) ) ;
#1638=DIRECTION ( 'NONE',  ( 1.000000000000000000, 0.000000000000000000, 0.000000000000000000 ) ) ;
#1642=CIRCLE ( 'NONE', #2024, 0.2000000000000005107 ) ;
#1655=ORIENTED_EDGE ( 'NONE', *, *, #14504, .T. ) ;
#1661=ORIENTED_EDGE ( 'NONE', *, *, #3484, .T. ) ;
#1696=AXIS2_PLACEMENT_3D ( 'NONE', #20506, #3629, #16465 ) ;
#1706=CARTESIAN_POINT ( 'NONE',  ( -1.506022603841296270, 0.000000000000000000, 0.000000000000000000 ) ) ;
#1779=DIRECTION ( 'NONE',  ( 1.000000000000000000, 0.000000000000000000, 0.000000000000000000 ) ) ;
#1787=FACE_OUTER_BOUND ( 'NONE', #15021, .T. ) ;
#1805=EDGE_LOOP ( 'NONE', ( #18352, #23211, #22697, #21151 ) ) ;
#1810=ORIENTED_EDGE ( 'NONE', *, *, #2201, .F. ) ;
#1822=AXIS2_PLACEMENT_3D ( 'NONE', #20393, #873, #8206 ) ;
#1849=CIRCLE ( 'NONE', #20210, 8.265000000000021885 ) ;
#1861=ORIENTED_EDGE ( 'NONE', *, *, #5688, .F. ) ;
#1877=CARTESIAN_POINT ( 'NONE',  ( -1.506022603841227436, 0.000000000000000000, 0.000000000000000000 ) ) ;
#1886=AXIS2_PLACEMENT_3D ( 'NONE', #16187, #10818, #12617 ) ;
#1901=EDGE_CURVE ( 'NONE', #11881, #10070, #12778, .T. ) ;
#1912=FILL_AREA_STYLE_COLOUR ( '', #12584 ) ;
#1950=CYLINDRICAL_SURFACE ( 'NONE', #8702, 8.265000000000021885 ) ;
#1971=DIRECTION ( 'NONE',  ( 0.000000000000000000, 0.000000000000000000, -1.000000000000000000 ) ) ;
#1987=AXIS2_PLACEMENT_3D ( 'NONE', #4169, #22358, #10062 ) ;
#1994=EDGE_CURVE ( 'NONE', #19611, #2045, #6256, .T. ) ;
#2024=AXIS2_PLACEMENT_3D ( 'NONE', #6122, #13326, #7925 ) ;
#2045=VERTEX_POINT ( 'NONE', #12029 ) ;
#2061=EDGE_CURVE ( 'NONE', #4680, #2595, #5100, .T. ) ;
#2072=CARTESIAN_POINT ( 'NONE',  ( 1.489200000000000079, 1.009010990753487416E-15, 8.239200000000002078 ) ) ;
#2076=ORIENTED_EDGE ( 'NONE', *, *, #21459, .F. ) ;
#2081=AXIS2_PLACEMENT_3D ( 'NONE', #3226, #8886, #16300 ) ;
#2104=AXIS2_PLACEMENT_3D ( 'NONE', #11305, #18579, #12014 ) ;
#2119=AXIS2_PLACEMENT_3D ( 'NONE', #17968, #1304, #23002 ) ;
#2120=CARTESIAN_POINT ( 'NONE',  ( -2.000000000000001776, 0.000000000000000000, 0.000000000000000000 ) ) ;
#2153=VERTEX_POINT ( 'NONE', #18097 ) ;
#2186=DIRECTION ( 'NONE',  ( 0.000000000000000000, 0.000000000000000000, -1.000000000000000000 ) ) ;
#2194=VERTEX_POINT ( 'NONE', #3625 ) ;
#2201=EDGE_CURVE ( 'NONE', #2045, #19611, #12396, .T. ) ;
#2212=STYLED_ITEM ( 'NONE', ( #12501 ), #14766 ) ;
#2226=DIRECTION ( 'NONE',  ( 1.000000000000000000, 0.000000000000000000, 0.000000000000000000 ) ) ;
#2249=VECTOR ( 'NONE', #20228, 1000.000000000000000 ) ;
#2334=EDGE_CURVE ( 'NONE', #892, #3058, #1642, .T. ) ;
#2376=AXIS2_PLACEMENT_3D ( 'NONE', #11979, #11861, #2723 ) ;
#2378=ORIENTED_EDGE ( 'NONE', *, *, #2925, .T. ) ;
#2407=CARTESIAN_POINT ( 'NONE',  ( 2.000000000000001776, 8.013782491920513601E-16, -6.543750000000017053 ) ) ;
#2429=VECTOR ( 'NONE', #16406, 1000.000000000000000 ) ;
#2462=ADVANCED_FACE ( 'NONE', ( #4786 ), #15845, .T. ) ;
#2468=ADVANCED_FACE ( 'NONE', ( #5141 ), #5875, .T. ) ;
#2473=CARTESIAN_POINT ( 'NONE',  ( -2.000000000000001776, 0.000000000000000000, 0.000000000000000000 ) ) ;
#2507=CARTESIAN_POINT ( 'NONE',  ( -2.000000000000001776, 0.000000000000000000, 0.000000000000000000 ) ) ;
#2513=CYLINDRICAL_SURFACE ( 'NONE', #8412, 8.073750000000021743 ) ;
#2520=VERTEX_POINT ( 'NONE', #19623 ) ;
#2567=DIRECTION ( 'NONE',  ( -0.000000000000000000, -1.000000000000000000, -0.000000000000000000 ) ) ;
#2579=AXIS2_PLACEMENT_3D ( 'NONE', #15914, #1163, #12339 ) ;
#2595=VERTEX_POINT ( 'NONE', #10451 ) ;
#2606=EDGE_LOOP ( 'NONE', ( #11060, #17510, #10663, #17349 ) ) ;
#2628=ORIENTED_EDGE ( 'NONE', *, *, #2925, .F. ) ;
#2647=ORIENTED_EDGE ( 'NONE', *, *, #10100, .F. ) ;
#2655=CONICAL_SURFACE ( 'NONE', #21006, 6.543750000000017053, 0.4459949661726622105 ) ;
#2671=EDGE_CURVE ( 'NONE', #23515, #16003, #20324, .T. ) ;
#2718=APPLICATION_CONTEXT ( 'automotive_design' ) ;
#2723=DIRECTION ( 'NONE',  ( 0.000000000000000000, 0.000000000000000000, -1.000000000000000000 ) ) ;
#2737=CARTESIAN_POINT ( 'NONE',  ( 1.600000000000004086, 0.000000000000000000, 0.000000000000000000 ) ) ;
#2751=FACE_OUTER_BOUND ( 'NONE', #19651, .T. ) ;
#2785=DIRECTION ( 'NONE',  ( 1.000000000000000000, 0.000000000000000000, 0.000000000000000000 ) ) ;
#2790=VERTEX_POINT ( 'NONE', #11743 ) ;
#2801=ADVANCED_FACE ( 'NONE', ( #13648 ), #15423, .T. ) ;
#2815=ORIENTED_EDGE ( 'NONE', *, *, #17717, .T. ) ;
#2830=DIRECTION ( 'NONE',  ( 0.000000000000000000, 0.000000000000000000, -1.000000000000000000 ) ) ;
#2835=ORIENTED_EDGE ( 'NONE', *, *, #6728, .F. ) ;
#2901=FACE_OUTER_BOUND ( 'NONE', #23052, .T. ) ;
#2925=EDGE_CURVE ( 'NONE', #3058, #2194, #5833, .T. ) ;
#2948=CARTESIAN_POINT ( 'NONE',  ( -1.799999999999996048, 1.102182119232620672E-15, 9.000000000000021316 ) ) ;
#2950=VECTOR ( 'NONE', #12805, 1000.000000000000000 ) ;
#2951=AXIS2_PLACEMENT_3D ( 'NONE', #15519, #11934, #15637 ) ;
#2956=DIRECTION ( 'NONE',  ( 0.000000000000000000, 0.000000000000000000, -1.000000000000000000 ) ) ;
#2989=FACE_OUTER_BOUND ( 'NONE', #6826, .T. ) ;
#3011=CARTESIAN_POINT ( 'NONE',  ( -1.520000000000000462, 1.010590785124388747E-15, 8.239200000000002078 ) ) ;
#3031=ADVANCED_FACE ( 'NONE', ( #21622 ), #8524, .T. ) ;
#3036=CIRCLE ( 'NONE', #11862, 8.239200000000002078 ) ;
#3056=PLANE ( 'NONE',  #18656 ) ;
#3058=VERTEX_POINT ( 'NONE', #13887 ) ;
#3059=CARTESIAN_POINT ( 'NONE',  ( 1.519999999999999352, 6.760799999999997034, 0.000000000000000000 ) ) ;
#3065=DIRECTION ( 'NONE',  ( 1.000000000000000000, 0.000000000000000000, 0.000000000000000000 ) ) ;
#3077=ADVANCED_FACE ( 'NONE', ( #1515, #3192 ), #12094, .T. ) ;
#3104=CARTESIAN_POINT ( 'NONE',  ( -1.600000000000004086, 9.887492094615969966E-16, 8.073750000000021743 ) ) ;
#3111=CARTESIAN_POINT ( 'NONE',  ( 0.000000000000000000, 0.000000000000000000, 0.000000000000000000 ) ) ;
#3141=DIRECTION ( 'NONE',  ( 1.000000000000000000, 0.000000000000000000, 0.000000000000000000 ) ) ;
#3160=CARTESIAN_POINT ( 'NONE',  ( -1.799999999999996048, 0.000000000000000000, -9.000000000000021316 ) ) ;
#3177=DIRECTION ( 'NONE',  ( 0.000000000000000000, 0.000000000000000000, -1.000000000000000000 ) ) ;
#3192=FACE_BOUND ( 'NONE', #1637, .T. ) ;
#3199=ORIENTED_EDGE ( 'NONE', *, *, #13220, .T. ) ;
#3226=CARTESIAN_POINT ( 'NONE',  ( -90.00000000000000000, 0.000000000000000000, 0.000000000000000000 ) ) ;
#3232=DIRECTION ( 'NONE',  ( 1.000000000000000000, 0.000000000000000000, 0.000000000000000000 ) ) ;
#3241=AXIS2_PLACEMENT_3D ( 'NONE', #14155, #12486, #5035 ) ;
#3259=ORIENTED_EDGE ( 'NONE', *, *, #19086, .T. ) ;
#3264=DIRECTION ( 'NONE',  ( 0.000000000000000000, 0.000000000000000000, -1.000000000000000000 ) ) ;
#3291=ORIENTED_EDGE ( 'NONE', *, *, #9103, .T. ) ;
#3315=CARTESIAN_POINT ( 'NONE',  ( -90.00000000000000000, 1.102182119232620672E-15, 9.000000000000021316 ) ) ;
#3341=CARTESIAN_POINT ( 'NONE',  ( 1.520000000000000462, 0.000000000000000000, 0.000000000000000000 ) ) ;
#3350=ORIENTED_EDGE ( 'NONE', *, *, #4830, .T. ) ;
#3351=DIRECTION ( 'NONE',  ( 0.000000000000000000, 0.000000000000000000, -1.000000000000000000 ) ) ;
#3358=DIRECTION ( 'NONE',  ( 1.000000000000000000, -0.000000000000000000, -0.000000000000000000 ) ) ;
#3365=AXIS2_PLACEMENT_3D ( 'NONE', #16417, #23697, #11527 ) ;
#3417=ORIENTED_EDGE ( 'NONE', *, *, #15818, .T. ) ;
#3421=ORIENTED_EDGE ( 'NONE', *, *, #7065, .F. ) ;
#3424=VECTOR ( 'NONE', #18387, 1000.000000000000000 ) ;
#3443=DIRECTION ( 'NONE',  ( 0.000000000000000000, 1.000000000000000000, -1.224646799147353207E-16 ) ) ;
#3447=AXIS2_PLACEMENT_3D ( 'NONE', #8852, #1628, #8972 ) ;
#3461=AXIS2_PLACEMENT_3D ( 'NONE', #21544, #17855, #9250 ) ;
#3470=DIRECTION ( 'NONE',  ( 0.000000000000000000, 0.000000000000000000, 1.000000000000000000 ) ) ;
#3484=EDGE_CURVE ( 'NONE', #2790, #15133, #20822, .T. ) ;
#3504=ADVANCED_FACE ( 'NONE', ( #1415 ), #12366, .F. ) ;
#3551=ORIENTED_EDGE ( 'NONE', *, *, #1434, .F. ) ;
#3568=DIRECTION ( 'NONE',  ( 1.000000000000000000, 0.000000000000000000, 0.000000000000000000 ) ) ;
#3584=ORIENTED_EDGE ( 'NONE', *, *, #9637, .T. ) ;
#3608=EDGE_CURVE ( 'NONE', #12123, #2153, #20444, .T. ) ;
#3622=ADVANCED_FACE ( 'NONE', ( #22362 ), #17419, .T. ) ;
#3624=ADVANCED_FACE ( 'NONE', ( #13300 ), #16638, .F. ) ;
#3625=CARTESIAN_POINT ( 'NONE',  ( 2.000000000000001776, 1.089935651241147118E-15, 8.800000000000023803 ) ) ;
#3628=DIRECTION ( 'NONE',  ( 1.000000000000000000, 0.000000000000000000, 0.000000000000000000 ) ) ;
#3629=DIRECTION ( 'NONE',  ( 1.000000000000000000, 0.000000000000000000, 0.000000000000000000 ) ) ;
#3673=DIRECTION ( 'NONE',  ( 0.000000000000000000, 0.000000000000000000, -1.000000000000000000 ) ) ;
#3714=CARTESIAN_POINT ( 'NONE',  ( -90.00000000000000000, 7.347880794884145374E-16, 6.000000000000021316 ) ) ;
#3725=AXIS2_PLACEMENT_3D ( 'NONE', #12394, #18668, #19659 ) ;
#3753=CARTESIAN_POINT ( 'NONE',  ( -1.600000000000004086, 0.000000000000000000, 0.000000000000000000 ) ) ;
#3758=PRODUCT_DEFINITION_SHAPE ( 'NONE', 'NONE',  #520 ) ;
#3759=EDGE_CURVE ( 'NONE', #19804, #10717, #10194, .T. ) ;
#3789=DIRECTION ( 'NONE',  ( 0.000000000000000000, 0.000000000000000000, -1.000000000000000000 ) ) ;
#3790=EDGE_LOOP ( 'NONE', ( #901, #7731, #8155, #9710 ) ) ;
#3805=DIRECTION ( 'NONE',  ( 0.000000000000000000, 0.000000000000000000, -1.000000000000000000 ) ) ;
#3829=CARTESIAN_POINT ( 'NONE',  ( -2.000000000000001776, 0.000000000000000000, 0.000000000000000000 ) ) ;
#3847=CARTESIAN_POINT ( 'NONE',  ( -1.800000000000000711, 1.077689183249673564E-15, 8.800000000000022027 ) ) ;
#3864=DIRECTION ( 'NONE',  ( 1.000000000000000000, 0.000000000000000000, 0.000000000000000000 ) ) ;
#3866=AXIS2_PLACEMENT_3D ( 'NONE', #20679, #8847, #10175 ) ;
#3870=CARTESIAN_POINT ( 'NONE',  ( 1.799999999999996048, 7.347880794884147346E-16, 6.000000000000023093 ) ) ;
#3970=CYLINDRICAL_SURFACE ( 'NONE', #2104, 9.000000000000021316 ) ;
#4009=AXIS2_PLACEMENT_3D ( 'NONE', #9123, #7677, #15105 ) ;
#4010=CARTESIAN_POINT ( 'NONE',  ( -90.00000000000000000, 9.887492094615969966E-16, 8.073750000000021743 ) ) ;
#4024=ORIENTED_EDGE ( 'NONE', *, *, #2061, .F. ) ;
#4164=DIRECTION ( 'NONE',  ( 1.000000000000000000, 0.000000000000000000, 0.000000000000000000 ) ) ;
#4169=CARTESIAN_POINT ( 'NONE',  ( -1.800000000000000711, 0.000000000000000000, 0.000000000000000000 ) ) ;
#4174=DIRECTION ( 'NONE',  ( 1.000000000000000000, 0.000000000000000000, 0.000000000000000000 ) ) ;
#4183=CIRCLE ( 'NONE', #8777, 6.000000000000021316 ) ;
#4231=CARTESIAN_POINT ( 'NONE',  ( -90.00000000000000000, 0.000000000000000000, 0.000000000000000000 ) ) ;
#4307=CARTESIAN_POINT ( 'NONE',  ( 2.000000000000001776, 0.000000000000000000, -8.073750000000021743 ) ) ;
#4319=CARTESIAN_POINT ( 'NONE',  ( -90.00000000000000000, 8.247996192257451316E-16, 6.735000000000022524 ) ) ;
#4350=SURFACE_STYLE_USAGE ( .BOTH. , #23521 ) ;
#4361=EDGE_CURVE ( 'NONE', #10070, #9347, #6267, .T. ) ;
#4381=ORIENTED_EDGE ( 'NONE', *, *, #3759, .F. ) ;
#4437=DIRECTION ( 'NONE',  ( 1.000000000000000000, 0.000000000000000000, 0.000000000000000000 ) ) ;
#4446=DIRECTION ( 'NONE',  ( 1.000000000000000000, 0.000000000000000000, 0.000000000000000000 ) ) ;
#4447=ORIENTED_EDGE ( 'NONE', *, *, #15114, .F. ) ;
#4470=EDGE_CURVE ( 'NONE', #19611, #8470, #480, .T. ) ;
#4519=AXIS2_PLACEMENT_3D ( 'NONE', #3753, #9413, #20392 ) ;
#4520=FACE_OUTER_BOUND ( 'NONE', #17875, .T. ) ;
#4523=MECHANICAL_DESIGN_GEOMETRIC_PRESENTATION_REPRESENTATION('',(#18302),#19055);
#4543=TOROIDAL_SURFACE ( 'NONE', #23671, 8.800000000000022027, 0.2000000000000011768 ) ;
#4599=AXIS2_PLACEMENT_3D ( 'NONE', #3847, #21912, #16550 ) ;
#4611=CIRCLE ( 'NONE', #18000, 8.073750000000021743 ) ;
#4622=ORIENTED_EDGE ( 'NONE', *, *, #9338, .T. ) ;
#4625=EDGE_LOOP ( 'NONE', ( #15397, #12308, #21653, #6134 ) ) ;
#4649=DIRECTION ( 'NONE',  ( 1.000000000000000000, 0.000000000000000000, 0.000000000000000000 ) ) ;
#4680=VERTEX_POINT ( 'NONE', #18454 ) ;
#4681=CARTESIAN_POINT ( 'NONE',  ( -90.00000000000000000, 1.012170579495290078E-15, 8.265000000000021885 ) ) ;
#4786=FACE_OUTER_BOUND ( 'NONE', #1805, .T. ) ;
#4830=EDGE_CURVE ( 'NONE', #2790, #12003, #13804, .T. ) ;
#4845=DIRECTION ( 'NONE',  ( 0.000000000000000000, 0.000000000000000000, -1.000000000000000000 ) ) ;
#4853=FACE_BOUND ( 'NONE', #16948, .T. ) ;
#4854=VECTOR ( 'NONE', #3628, 1000.000000000000000 ) ;
#4859=APPLICATION_CONTEXT ( 'automotive_design' ) ;
#4883=DIRECTION ( 'NONE',  ( 1.000000000000000000, -0.000000000000000000, -0.000000000000000000 ) ) ;
#4925=CARTESIAN_POINT ( 'NONE',  ( -2.000000000000001776, 0.000000000000000000, 0.000000000000000000 ) ) ;
#4946=VERTEX_POINT ( 'NONE', #17378 ) ;
#4947=FACE_OUTER_BOUND ( 'NONE', #11013, .T. ) ;
#4967=ADVANCED_FACE ( 'NONE', ( #6482 ), #718, .T. ) ;
#4969=DIRECTION ( 'NONE',  ( -1.000000000000000000, 0.000000000000000000, 0.000000000000000000 ) ) ;
#5003=DIRECTION ( 'NONE',  ( -0.000000000000000000, 0.000000000000000000, 1.000000000000000000 ) ) ;
#5030=CARTESIAN_POINT ( 'NONE',  ( -1.800000000000000711, 0.000000000000000000, 0.000000000000000000 ) ) ;
#5035=DIRECTION ( 'NONE',  ( 0.000000000000000000, 0.000000000000000000, 1.000000000000000000 ) ) ;
#5044=CARTESIAN_POINT ( 'NONE',  ( 2.000000000000001776, 0.000000000000000000, 0.000000000000000000 ) ) ;
#5100=CIRCLE ( 'NONE', #14689, 6.543750000000017053 ) ;
#5128=VERTEX_POINT ( 'NONE', #2948 ) ;
#5141=FACE_OUTER_BOUND ( 'NONE', #861, .T. ) ;
#5229=CARTESIAN_POINT ( 'NONE',  ( -1.600000000000004086, 0.000000000000000000, 0.000000000000000000 ) ) ;
#5283=AXIS2_PLACEMENT_3D ( 'NONE', #5400, #10929, #14643 ) ;
#5309=CIRCLE ( 'NONE', #8388, 8.239200000000002078 ) ;
#5399=ADVANCED_FACE ( 'NONE', ( #15909, #23186 ), #16148, .T. ) ;
#5400=CARTESIAN_POINT ( 'NONE',  ( -2.000000000000001776, 0.000000000000000000, 0.000000000000000000 ) ) ;
#5431=DIRECTION ( 'NONE',  ( 1.000000000000000000, 0.000000000000000000, 0.000000000000000000 ) ) ;
#5456=CARTESIAN_POINT ( 'NONE',  ( -1.489200000000000301, 0.000000000000000000, -8.239200000000002078 ) ) ;
#5532=ORIENTED_EDGE ( 'NONE', *, *, #3608, .T. ) ;
#5549=ORIENTED_EDGE ( 'NONE', *, *, #8261, .T. ) ;
#5578=DIRECTION ( 'NONE',  ( 1.000000000000000000, -0.000000000000000000, -0.000000000000000000 ) ) ;
#5590=EDGE_CURVE ( 'NONE', #701, #9988, #1078, .T. ) ;
#5594=CARTESIAN_POINT ( 'NONE',  ( -1.800000000000000711, 0.000000000000000000, 0.000000000000000000 ) ) ;
#5630=FILL_AREA_STYLE ('',( #1912 ) ) ;
#5651=AXIS2_PLACEMENT_3D ( 'NONE', #7047, #4883, #2956 ) ;
#5671=CYLINDRICAL_SURFACE ( 'NONE', #1696, 6.735000000000022524 ) ;
#5688=EDGE_CURVE ( 'NONE', #2520, #12003, #20136, .T. ) ;
#5779=ORIENTED_EDGE ( 'NONE', *, *, #17180, .T. ) ;
#5833=CIRCLE ( 'NONE', #2376, 8.800000000000023803 ) ;
#5834=EDGE_CURVE ( 'NONE', #2595, #4680, #10298, .T. ) ;
#5863=CARTESIAN_POINT ( 'NONE',  ( 1.600000000000004086, 0.000000000000000000, 0.000000000000000000 ) ) ;
#5875=TOROIDAL_SURFACE ( 'NONE', #521, 6.200000000000020606, 0.1999999999999997613 ) ;
#5913=FACE_OUTER_BOUND ( 'NONE', #14977, .T. ) ;
#5923=ADVANCED_FACE ( 'NONE', ( #19138 ), #6784, .T. ) ;
#5961=VECTOR ( 'NONE', #4437, 1000.000000000000000 ) ;
#5970=EDGE_LOOP ( 'NONE', ( #11130, #11714, #15199, #78 ) ) ;
#5992=CARTESIAN_POINT ( 'NONE',  ( -2.000000000000001776, 9.887492094615969966E-16, 8.073750000000021743 ) ) ;
#6003=VERTEX_POINT ( 'NONE', #16268 ) ;
#6031=EDGE_CURVE ( 'NONE', #5128, #16266, #1385, .T. ) ;
#6048=DIRECTION ( 'NONE',  ( 1.000000000000000000, -0.000000000000000000, -0.000000000000000000 ) ) ;
#6084=ORIENTED_EDGE ( 'NONE', *, *, #1335, .F. ) ;
#6089=AXIS2_PLACEMENT_3D ( 'NONE', #9613, #9141, #19992 ) ;
#6091=CIRCLE ( 'NONE', #17956, 6.735000000000022524 ) ;
#6093=CARTESIAN_POINT ( 'NONE',  ( 2.000000000000001776, 0.000000000000000000, 0.000000000000000000 ) ) ;
#6109=VECTOR ( 'NONE', #20188, 999.9999999999998863 ) ;
#6122=CARTESIAN_POINT ( 'NONE',  ( 1.799999999999999600, 0.000000000000000000, -8.800000000000023803 ) ) ;
#6134=ORIENTED_EDGE ( 'NONE', *, *, #302, .F. ) ;
#6136=VECTOR ( 'NONE', #19441, 1000.000000000000114 ) ;
#6169=EDGE_LOOP ( 'NONE', ( #13713, #11260 ) ) ;
#6234=DIRECTION ( 'NONE',  ( 0.000000000000000000, 0.000000000000000000, -1.000000000000000000 ) ) ;
#6256=CIRCLE ( 'NONE', #19621, 6.735000000000022524 ) ;
#6267=LINE ( 'NONE', #12143, #22721 ) ;
#6303=ORIENTED_EDGE ( 'NONE', *, *, #1393, .T. ) ;
#6320=VECTOR ( 'NONE', #6593, 1000.000000000000000 ) ;
#6328=DIRECTION ( 'NONE',  ( 0.000000000000000000, 0.000000000000000000, -1.000000000000000000 ) ) ;
#6330=CARTESIAN_POINT ( 'NONE',  ( 1.799999999999999156, 0.000000000000000000, 0.000000000000000000 ) ) ;
#6365=EDGE_CURVE ( 'NONE', #9347, #14277, #14078, .T. ) ;
#6388=ORIENTED_EDGE ( 'NONE', *, *, #5688, .T. ) ;
#6414=AXIS2_PLACEMENT_3D ( 'NONE', #7360, #8919, #16213 ) ;
#6428=CARTESIAN_POINT ( 'NONE',  ( 2.000000000000001776, 0.000000000000000000, 0.000000000000000000 ) ) ;
#6450=COLOUR_RGB ( '', 0.08235294, 0.09019608, 0.10196078) ;
#6453=ORIENTED_EDGE ( 'NONE', *, *, #1272, .F. ) ;
#6482=FACE_OUTER_BOUND ( 'NONE', #17566, .T. ) ;
#6485=CYLINDRICAL_SURFACE ( 'NONE', #23270, 6.000000000000021316 ) ;
#6490=AXIS2_PLACEMENT_3D ( 'NONE', #3059, #8705, #10405 ) ;
#6544=ADVANCED_FACE ( 'NONE', ( #10514, #19812 ), #14334, .T. ) ;
#6548=ORIENTED_EDGE ( 'NONE', *, *, #6031, .T. ) ;
#6556=FACE_OUTER_BOUND ( 'NONE', #22102, .T. ) ;
#6573=DIRECTION ( 'NONE',  ( 0.000000000000000000, 0.000000000000000000, -1.000000000000000000 ) ) ;
#6578=FACE_OUTER_BOUND ( 'NONE', #21947, .T. ) ;
#6580=CARTESIAN_POINT ( 'NONE',  ( -1.520000000000000462, 0.000000000000000000, 0.000000000000000000 ) ) ;
#6588=CARTESIAN_POINT ( 'NONE',  ( 1.799999999999999156, 0.000000000000000000, 0.000000000000000000 ) ) ;
#6593=DIRECTION ( 'NONE',  ( 1.000000000000000000, 0.000000000000000000, 0.000000000000000000 ) ) ;
#6609=ORIENTED_EDGE ( 'NONE', *, *, #18290, .T. ) ;
#6610=ADVANCED_FACE ( 'NONE', ( #4853, #19461 ), #3056, .T. ) ;
#6640=CARTESIAN_POINT ( 'NONE',  ( -90.00000000000000000, 0.000000000000000000, 0.000000000000000000 ) ) ;
#6653=AXIS2_PLACEMENT_3D ( 'NONE', #10332, #6824, #23214 ) ;
#6666=VERTEX_POINT ( 'NONE', #9188 ) ;
#6702=EDGE_CURVE ( 'NONE', #23515, #6003, #21317, .T. ) ;
#6708=ORIENTED_EDGE ( 'NONE', *, *, #4361, .T. ) ;
#6711=CIRCLE ( 'NONE', #7091, 0.1999999999999996503 ) ;
#6728=EDGE_CURVE ( 'NONE', #17331, #10854, #14481, .T. ) ;
#6750=LINE ( 'NONE', #8673, #15258 ) ;
#6784=TOROIDAL_SURFACE ( 'NONE', #700, 8.239200000000002078, 0.03079999999999879709 ) ;
#6786=ADVANCED_FACE ( 'NONE', ( #16831 ), #7597, .T. ) ;
#6798=CARTESIAN_POINT ( 'NONE',  ( -2.000000000000000888, 6.543750000000021494, 0.000000000000000000 ) ) ;
#6824=DIRECTION ( 'NONE',  ( 1.000000000000000000, -0.000000000000000000, -0.000000000000000000 ) ) ;
#6826=EDGE_LOOP ( 'NONE', ( #570, #14219, #20776, #20249 ) ) ;
#6841=FACE_OUTER_BOUND ( 'NONE', #15409, .T. ) ;
#6843=DIRECTION ( 'NONE',  ( 1.000000000000000000, 0.000000000000000000, 0.000000000000000000 ) ) ;
#6898=DIRECTION ( 'NONE',  ( 1.000000000000000000, -0.000000000000000000, -0.000000000000000000 ) ) ;
#6910=AXIS2_PLACEMENT_3D ( 'NONE', #9605, #16534, #9357 ) ;
#6912=VECTOR ( 'NONE', #11295, 1000.000000000000000 ) ;
#6935=EDGE_LOOP ( 'NONE', ( #19729, #12947, #1368, #1018 ) ) ;
#6994=ADVANCED_FACE ( 'NONE', ( #4947 ), #13841, .F. ) ;
#7007=ORIENTED_EDGE ( 'NONE', *, *, #5834, .F. ) ;
#7038=EDGE_CURVE ( 'NONE', #19003, #892, #6750, .T. ) ;
#7043=DIRECTION ( 'NONE',  ( 1.000000000000000000, 0.000000000000000000, 0.000000000000000000 ) ) ;
#7047=CARTESIAN_POINT ( 'NONE',  ( -1.489200000000000301, 0.000000000000000000, 0.000000000000000000 ) ) ;
#7065=EDGE_CURVE ( 'NONE', #23109, #6666, #12592, .T. ) ;
#7088=AXIS2_PLACEMENT_3D ( 'NONE', #9350, #341, #18667 ) ;
#7091=AXIS2_PLACEMENT_3D ( 'NONE', #12907, #21856, #14470 ) ;
#7110=VECTOR ( 'NONE', #4446, 1000.000000000000000 ) ;
#7154=CARTESIAN_POINT ( 'NONE',  ( -2.000000000000001776, 0.000000000000000000, -8.800000000000022027 ) ) ;
#7190=AXIS2_PLACEMENT_3D ( 'NONE', #19015, #13538, #11523 ) ;
#7207=LINE ( 'NONE', #12253, #20170 ) ;
#7214=DIRECTION ( 'NONE',  ( -1.000000000000000000, 0.000000000000000000, 0.000000000000000000 ) ) ;
#7221=CIRCLE ( 'NONE', #3365, 8.265000000000021885 ) ;
#7225=AXIS2_PLACEMENT_3D ( 'NONE', #6640, #991, #8800 ) ;
#7254=FACE_OUTER_BOUND ( 'NONE', #18173, .T. ) ;
#7258=( LENGTH_UNIT ( ) NAMED_UNIT ( * ) SI_UNIT ( .MILLI., .METRE. ) );
#7266=DIRECTION ( 'NONE',  ( 0.000000000000000000, 0.000000000000000000, 1.000000000000000000 ) ) ;
#7297=ORIENTED_EDGE ( 'NONE', *, *, #1901, .F. ) ;
#7309=EDGE_CURVE ( 'NONE', #14277, #9347, #15629, .T. ) ;
#7318=AXIS2_PLACEMENT_3D ( 'NONE', #3111, #10686, #17843 ) ;
#7327=VERTEX_POINT ( 'NONE', #20806 ) ;
#7338=SURFACE_STYLE_USAGE ( .BOTH. , #8769 ) ;
#7353=EDGE_LOOP ( 'NONE', ( #21057, #14903 ) ) ;
#7360=CARTESIAN_POINT ( 'NONE',  ( -1.489200000000000079, 0.000000000000000000, 0.000000000000000000 ) ) ;
#7397=EDGE_CURVE ( 'NONE', #12358, #8470, #21301, .T. ) ;
#7406=ORIENTED_EDGE ( 'NONE', *, *, #14371, .T. ) ;
#7465=EDGE_CURVE ( 'NONE', #892, #16266, #11022, .T. ) ;
#7489=AXIS2_PLACEMENT_3D ( 'NONE', #10454, #12010, #8527 ) ;
#7492=EDGE_CURVE ( 'NONE', #19414, #7327, #23230, .T. ) ;
#7501=ADVANCED_FACE ( 'NONE', ( #6578 ), #9112, .T. ) ;
#7503=EDGE_CURVE ( 'NONE', #23245, #9804, #10260, .T. ) ;
#7556=TOROIDAL_SURFACE ( 'NONE', #14073, 8.239200000000002078, 0.03079999999999868954 ) ;
#7597=CONICAL_SURFACE ( 'NONE', #8356, 6.543750000000017053, 0.4459949661726622105 ) ;
#7656=CARTESIAN_POINT ( 'NONE',  ( 1.600000000000004086, 1.012170579495290078E-15, 8.265000000000021885 ) ) ;
#7672=TOROIDAL_SURFACE ( 'NONE', #18368, 6.200000000000021494, 0.1999999999999996503 ) ;
#7674=ORIENTED_EDGE ( 'NONE', *, *, #15078, .T. ) ;
#7677=DIRECTION ( 'NONE',  ( 1.000000000000000000, 0.000000000000000000, 0.000000000000000000 ) ) ;
#7691=DIRECTION ( 'NONE',  ( 0.000000000000000000, 0.000000000000000000, -1.000000000000000000 ) ) ;
#7731=ORIENTED_EDGE ( 'NONE', *, *, #1434, .T. ) ;
#7797=DIRECTION ( 'NONE',  ( 1.000000000000000000, 0.000000000000000000, 0.000000000000000000 ) ) ;
#7821=ORIENTED_EDGE ( 'NONE', *, *, #9071, .T. ) ;
#7857=AXIS2_PLACEMENT_3D ( 'NONE', #9584, #4164, #11511 ) ;
#7863=PLANE ( 'NONE',  #21227 ) ;
#7875=PRODUCT_DEFINITION_CONTEXT ( 'detailed design', #2718, 'design' ) ;
#7876=AXIS2_PLACEMENT_3D ( 'NONE', #22878, #11667, #17153 ) ;
#7883=AXIS2_PLACEMENT_3D ( 'NONE', #6798, #21382, #5003 ) ;
#7925=DIRECTION ( 'NONE',  ( 0.000000000000000000, 0.000000000000000000, -1.000000000000000000 ) ) ;
#7961=PRESENTATION_STYLE_ASSIGNMENT (( #4350 ) ) ;
#7995=AXIS2_PLACEMENT_3D ( 'NONE', #9705, #4174, #572 ) ;
#7996=DIRECTION ( 'NONE',  ( 0.000000000000000000, 0.000000000000000000, -1.000000000000000000 ) ) ;
#8000=TOROIDAL_SURFACE ( 'NONE', #8770, 8.800000000000023803, 0.2000000000000000944 ) ;
#8012=CYLINDRICAL_SURFACE ( 'NONE', #7857, 8.265000000000021885 ) ;
#8039=DIRECTION ( 'NONE',  ( 1.000000000000000000, 0.000000000000000000, 0.000000000000000000 ) ) ;
#8045=CARTESIAN_POINT ( 'NONE',  ( 1.799999999999999600, 0.000000000000000000, 0.000000000000000000 ) ) ;
#8054=DIRECTION ( 'NONE',  ( 1.000000000000000000, 0.000000000000000000, 0.000000000000000000 ) ) ;
#8079=EDGE_CURVE ( 'NONE', #19075, #15133, #10284, .T. ) ;
#8149=EDGE_LOOP ( 'NONE', ( #5532, #9435, #17962, #13430 ) ) ;
#8155=ORIENTED_EDGE ( 'NONE', *, *, #11296, .T. ) ;
#8169=DIRECTION ( 'NONE',  ( 1.000000000000000000, 0.000000000000000000, 0.000000000000000000 ) ) ;
#8206=DIRECTION ( 'NONE',  ( 0.000000000000000000, 0.000000000000000000, -1.000000000000000000 ) ) ;
#8244=CIRCLE ( 'NONE', #178, 6.200000000000020606 ) ;
#8250=CARTESIAN_POINT ( 'NONE',  ( 1.506022603841296714, 0.000000000000000000, 0.000000000000000000 ) ) ;
#8261=EDGE_CURVE ( 'NONE', #4946, #22848, #8369, .T. ) ;
#8275=VECTOR ( 'NONE', #13461, 999.9999999999998863 ) ;
#8309=ORIENTED_EDGE ( 'NONE', *, *, #2334, .T. ) ;
#8320=AXIS2_PLACEMENT_3D ( 'NONE', #4925, #6843, #19881 ) ;
#8323=AXIS2_PLACEMENT_3D ( 'NONE', #23175, #3065, #3177 ) ;
#8329=ADVANCED_FACE ( 'NONE', ( #2901 ), #17423, .T. ) ;
#8349=CIRCLE ( 'NONE', #16005, 6.000000000000021316 ) ;
#8356=AXIS2_PLACEMENT_3D ( 'NONE', #15054, #20514, #7266 ) ;
#8369=CIRCLE ( 'NONE', #11443, 6.000000000000022204 ) ;
#8378=DIRECTION ( 'NONE',  ( 0.000000000000000000, 0.000000000000000000, -1.000000000000000000 ) ) ;
#8388=AXIS2_PLACEMENT_3D ( 'NONE', #6580, #19722, #8505 ) ;
#8409=CARTESIAN_POINT ( 'NONE',  ( 1.506022603841227436, 1.012170579495290078E-15, 8.265000000000021885 ) ) ;
#8412=AXIS2_PLACEMENT_3D ( 'NONE', #10091, #8169, #22870 ) ;
#8420=ORIENTED_EDGE ( 'NONE', *, *, #15114, .T. ) ;
#8447=CIRCLE ( 'NONE', #3447, 8.239200000000002078 ) ;
#8457=CARTESIAN_POINT ( 'NONE',  ( 1.506022603841296714, 0.000000000000000000, -6.735000000000022524 ) ) ;
#8470=VERTEX_POINT ( 'NONE', #23386 ) ;
#8493=CARTESIAN_POINT ( 'NONE',  ( -1.600000000000004086, 0.000000000000000000, 0.000000000000000000 ) ) ;
#8505=DIRECTION ( 'NONE',  ( 0.000000000000000000, 0.000000000000000000, -1.000000000000000000 ) ) ;
#8508=ADVANCED_FACE ( 'NONE', ( #21692 ), #20137, .T. ) ;
#8524=CONICAL_SURFACE ( 'NONE', #11595, 6.735000000000022524, 0.4459949661726533843 ) ;
#8527=DIRECTION ( 'NONE',  ( 0.000000000000000000, 0.000000000000000000, -1.000000000000000000 ) ) ;
#8528=ORIENTED_EDGE ( 'NONE', *, *, #13220, .F. ) ;
#8548=EDGE_LOOP ( 'NONE', ( #15549, #16893 ) ) ;
#8588=UNCERTAINTY_MEASURE_WITH_UNIT (LENGTH_MEASURE( 1.000000000000000082E-05 ), #14527, 'distance_accuracy_value', 'NONE');
#8602=CARTESIAN_POINT ( 'NONE',  ( -1.800000000000000711, 0.000000000000000000, -8.800000000000022027 ) ) ;
#8644=ORIENTED_EDGE ( 'NONE', *, *, #16909, .T. ) ;
#8651=CONICAL_SURFACE ( 'NONE', #21950, 6.735000000000022524, 0.4459949661726533843 ) ;
#8673=CARTESIAN_POINT ( 'NONE',  ( -90.00000000000000000, 0.000000000000000000, -9.000000000000021316 ) ) ;
#8702=AXIS2_PLACEMENT_3D ( 'NONE', #9288, #14802, #2186 ) ;
#8705=DIRECTION ( 'NONE',  ( 1.000000000000000000, 0.000000000000000000, -0.000000000000000000 ) ) ;
#8722=AXIS2_PLACEMENT_3D ( 'NONE', #6428, #20665, #7996 ) ;
#8737=CARTESIAN_POINT ( 'NONE',  ( -2.000000000000001776, 0.000000000000000000, -8.073750000000021743 ) ) ;
#8762=CARTESIAN_POINT ( 'NONE',  ( 2.000000000000001776, 9.887492094615969966E-16, 8.073750000000021743 ) ) ;
#8769=SURFACE_SIDE_STYLE ('',( #16075 ) ) ;
#8770=AXIS2_PLACEMENT_3D ( 'NONE', #8045, #20706, #11649 ) ;
#8777=AXIS2_PLACEMENT_3D ( 'NONE', #13516, #2226, #13402 ) ;
#8800=DIRECTION ( 'NONE',  ( 0.000000000000000000, 0.000000000000000000, -1.000000000000000000 ) ) ;
#8807=DIRECTION ( 'NONE',  ( 1.000000000000000000, -0.000000000000000000, -0.000000000000000000 ) ) ;
#8847=DIRECTION ( 'NONE',  ( 0.000000000000000000, -1.000000000000000000, 0.000000000000000000 ) ) ;
#8852=CARTESIAN_POINT ( 'NONE',  ( -1.520000000000000462, 0.000000000000000000, 0.000000000000000000 ) ) ;
#8854=DIRECTION ( 'NONE',  ( 1.000000000000000000, 0.000000000000000000, 0.000000000000000000 ) ) ;
#8858=CARTESIAN_POINT ( 'NONE',  ( -1.489200000000000301, 1.009010990753487416E-15, 8.239200000000002078 ) ) ;
#8861=ORIENTED_EDGE ( 'NONE', *, *, #9103, .F. ) ;
#8872=CARTESIAN_POINT ( 'NONE',  ( -1.600000000000004086, 0.000000000000000000, 0.000000000000000000 ) ) ;
#8886=DIRECTION ( 'NONE',  ( 1.000000000000000000, 0.000000000000000000, 0.000000000000000000 ) ) ;
#8913=ADVANCED_FACE ( 'NONE', ( #6841 ), #15618, .F. ) ;
#8919=DIRECTION ( 'NONE',  ( 1.000000000000000000, -0.000000000000000000, -0.000000000000000000 ) ) ;
#8921=AXIS2_PLACEMENT_3D ( 'NONE', #1322, #19296, #10114 ) ;
#8942=SURFACE_STYLE_FILL_AREA ( #18026 ) ;
#8950=EDGE_LOOP ( 'NONE', ( #18629, #22250, #12427, #1069 ) ) ;
#8972=DIRECTION ( 'NONE',  ( 0.000000000000000000, 0.000000000000000000, -1.000000000000000000 ) ) ;
#8998=EDGE_LOOP ( 'NONE', ( #17680, #13478 ) ) ;
#9059=FACE_OUTER_BOUND ( 'NONE', #11924, .T. ) ;
#9069=ADVANCED_FACE ( 'NONE', ( #18440, #1787 ), #10928, .T. ) ;
#9071=EDGE_CURVE ( 'NONE', #2045, #12358, #17593, .T. ) ;
#9103=EDGE_CURVE ( 'NONE', #9988, #6003, #3036, .T. ) ;
#9112=TOROIDAL_SURFACE ( 'NONE', #5651, 8.239200000000002078, 0.03079999999999868954 ) ;
#9115=CARTESIAN_POINT ( 'NONE',  ( 1.506022603841227436, 0.000000000000000000, -8.265000000000021885 ) ) ;
#9123=CARTESIAN_POINT ( 'NONE',  ( 2.000000000000001776, 0.000000000000000000, 0.000000000000000000 ) ) ;
#9141=DIRECTION ( 'NONE',  ( 0.000000000000000000, 1.000000000000000000, -1.224646799147353207E-16 ) ) ;
#9152=ORIENTED_EDGE ( 'NONE', *, *, #13877, .T. ) ;
#9188=CARTESIAN_POINT ( 'NONE',  ( -1.600000000000004086, 8.247996192257451316E-16, 6.735000000000022524 ) ) ;
#9217=FACE_OUTER_BOUND ( 'NONE', #21169, .T. ) ;
#9250=DIRECTION ( 'NONE',  ( 0.000000000000000000, 0.000000000000000000, -1.000000000000000000 ) ) ;
#9257=LINE ( 'NONE', #18213, #2249 ) ;
#9288=CARTESIAN_POINT ( 'NONE',  ( -90.00000000000000000, 0.000000000000000000, 0.000000000000000000 ) ) ;
#9331=AXIS2_PLACEMENT_3D ( 'NONE', #11157, #1779, #20092 ) ;
#9338=EDGE_CURVE ( 'NONE', #16266, #892, #22546, .T. ) ;
#9347=VERTEX_POINT ( 'NONE', #4307 ) ;
#9350=CARTESIAN_POINT ( 'NONE',  ( 1.799999999999999600, 0.000000000000000000, 0.000000000000000000 ) ) ;
#9357=DIRECTION ( 'NONE',  ( 0.000000000000000000, 0.000000000000000000, -1.000000000000000000 ) ) ;
#9413=DIRECTION ( 'NONE',  ( 1.000000000000000000, 0.000000000000000000, 0.000000000000000000 ) ) ;
#9430=ORIENTED_EDGE ( 'NONE', *, *, #15710, .F. ) ;
#9435=ORIENTED_EDGE ( 'NONE', *, *, #10609, .T. ) ;
#9454=DIRECTION ( 'NONE',  ( 1.000000000000000000, 0.000000000000000000, 0.000000000000000000 ) ) ;
#9531=VERTEX_POINT ( 'NONE', #21045 ) ;
#9584=CARTESIAN_POINT ( 'NONE',  ( -90.00000000000000000, 0.000000000000000000, 0.000000000000000000 ) ) ;
#9605=CARTESIAN_POINT ( 'NONE',  ( 1.600000000000004086, 0.000000000000000000, 0.000000000000000000 ) ) ;
#9606=DIRECTION ( 'NONE',  ( 0.000000000000000000, 0.000000000000000000, -1.000000000000000000 ) ) ;
#9613=CARTESIAN_POINT ( 'NONE',  ( 1.799999999999999156, 7.592810154713616459E-16, 6.200000000000021494 ) ) ;
#9637=EDGE_CURVE ( 'NONE', #4680, #12003, #10898, .T. ) ;
#9658=ORIENTED_EDGE ( 'NONE', *, *, #7065, .T. ) ;
#9675=DIRECTION ( 'NONE',  ( 0.000000000000000000, 0.000000000000000000, -1.000000000000000000 ) ) ;
#9683=EDGE_CURVE ( 'NONE', #7327, #22486, #23319, .T. ) ;
#9705=CARTESIAN_POINT ( 'NONE',  ( 1.600000000000004086, 0.000000000000000000, 0.000000000000000000 ) ) ;
#9710=ORIENTED_EDGE ( 'NONE', *, *, #14956, .F. ) ;
#9730=LINE ( 'NONE', #4319, #22594 ) ;
#9754=DIRECTION ( 'NONE',  ( 0.000000000000000000, 0.000000000000000000, -1.000000000000000000 ) ) ;
#9798=UNCERTAINTY_MEASURE_WITH_UNIT (LENGTH_MEASURE( 1.000000000000000082E-05 ), #11687, 'distance_accuracy_value', 'NONE');
#9804=VERTEX_POINT ( 'NONE', #199 ) ;
#9822=DIRECTION ( 'NONE',  ( 0.000000000000000000, 0.000000000000000000, -1.000000000000000000 ) ) ;
#9855=EDGE_LOOP ( 'NONE', ( #5779, #19625 ) ) ;
#9936=LINE ( 'NONE', #10420, #16294 ) ;
#9939=FACE_OUTER_BOUND ( 'NONE', #8149, .T. ) ;
#9957=ORIENTED_EDGE ( 'NONE', *, *, #9637, .F. ) ;
#9988=VERTEX_POINT ( 'NONE', #15150 ) ;
#10016=CARTESIAN_POINT ( 'NONE',  ( -90.00000000000000000, 0.000000000000000000, 0.000000000000000000 ) ) ;
#10062=DIRECTION ( 'NONE',  ( 0.000000000000000000, 0.000000000000000000, -1.000000000000000000 ) ) ;
#10070=VERTEX_POINT ( 'NONE', #20129 ) ;
#10091=CARTESIAN_POINT ( 'NONE',  ( -90.00000000000000000, 0.000000000000000000, 0.000000000000000000 ) ) ;
#10100=EDGE_CURVE ( 'NONE', #19003, #5128, #1137, .T. ) ;
#10114=DIRECTION ( 'NONE',  ( 0.000000000000000000, 1.224646799147367998E-16, 1.000000000000000000 ) ) ;
#10175=DIRECTION ( 'NONE',  ( 0.000000000000000000, 0.000000000000000000, -1.000000000000000000 ) ) ;
#10183=VERTEX_POINT ( 'NONE', #19291 ) ;
#10191=ORIENTED_EDGE ( 'NONE', *, *, #23395, .T. ) ;
#10194=CIRCLE ( 'NONE', #11342, 0.1999999999999996503 ) ;
#10195=AXIS2_PLACEMENT_3D ( 'NONE', #18925, #8054, #17267 ) ;
#10208=ORIENTED_EDGE ( 'NONE', *, *, #17979, .T. ) ;
#10212=DIRECTION ( 'NONE',  ( 1.000000000000000000, 0.000000000000000000, 0.000000000000000000 ) ) ;
#10223=CARTESIAN_POINT ( 'NONE',  ( -90.00000000000000000, 0.000000000000000000, 0.000000000000000000 ) ) ;
#10260=CIRCLE ( 'NONE', #13316, 6.543750000000021494 ) ;
#10284=CIRCLE ( 'NONE', #1822, 0.03079999999999923077 ) ;
#10298=CIRCLE ( 'NONE', #11006, 6.543750000000017053 ) ;
#10321=DIRECTION ( 'NONE',  ( 0.000000000000000000, 0.000000000000000000, -1.000000000000000000 ) ) ;
#10332=CARTESIAN_POINT ( 'NONE',  ( 1.489200000000000079, 0.000000000000000000, 0.000000000000000000 ) ) ;
#10402=CARTESIAN_POINT ( 'NONE',  ( 1.599999999999998979, 8.073750000000021743, 0.000000000000000000 ) ) ;
#10405=DIRECTION ( 'NONE',  ( -0.000000000000000000, 0.000000000000000000, -1.000000000000000000 ) ) ;
#10420=CARTESIAN_POINT ( 'NONE',  ( -90.00000000000000000, 0.000000000000000000, -6.735000000000022524 ) ) ;
#10451=CARTESIAN_POINT ( 'NONE',  ( 2.000000000000001776, 8.130889342088981965E-16, -6.543750000000017053 ) ) ;
#10454=CARTESIAN_POINT ( 'NONE',  ( 1.999999999999999112, 8.800000000000023803, 0.000000000000000000 ) ) ;
#10457=CARTESIAN_POINT ( 'NONE',  ( -1.520000000000000462, 0.000000000000000000, 0.000000000000000000 ) ) ;
#10498=AXIS2_PLACEMENT_3D ( 'NONE', #5456, #16839, #13138 ) ;
#10503=FACE_OUTER_BOUND ( 'NONE', #12857, .T. ) ;
#10508=ORIENTED_EDGE ( 'NONE', *, *, #14245, .F. ) ;
#10514=FACE_BOUND ( 'NONE', #6169, .T. ) ;
#10550=TOROIDAL_SURFACE ( 'NONE', #1336, 8.239200000000002078, 0.03079999999999879709 ) ;
#10556=ORIENTED_EDGE ( 'NONE', *, *, #1272, .T. ) ;
#10563=EDGE_CURVE ( 'NONE', #701, #9531, #9257, .T. ) ;
#10609=EDGE_CURVE ( 'NONE', #2153, #22848, #23278, .T. ) ;
#10616=DIRECTION ( 'NONE',  ( 0.000000000000000000, 0.000000000000000000, -1.000000000000000000 ) ) ;
#10623=DIRECTION ( 'NONE',  ( 0.000000000000000000, 0.000000000000000000, -1.000000000000000000 ) ) ;
#10661=VERTEX_POINT ( 'NONE', #5992 ) ;
#10662=DIRECTION ( 'NONE',  ( 1.000000000000000000, 0.000000000000000000, 0.000000000000000000 ) ) ;
#10663=ORIENTED_EDGE ( 'NONE', *, *, #6728, .T. ) ;
#10686=DIRECTION ( 'NONE',  ( 0.000000000000000000, 0.000000000000000000, 1.000000000000000000 ) ) ;
#10717=VERTEX_POINT ( 'NONE', #20932 ) ;
#10733=ADVANCED_FACE ( 'NONE', ( #19155 ), #8000, .T. ) ;
#10757=ORIENTED_EDGE ( 'NONE', *, *, #21797, .T. ) ;
#10791=CARTESIAN_POINT ( 'NONE',  ( 1.799999999999999600, 1.077689183249673761E-15, 8.800000000000023803 ) ) ;
#10818=DIRECTION ( 'NONE',  ( -0.000000000000000000, -1.000000000000000000, -0.000000000000000000 ) ) ;
#10829=CARTESIAN_POINT ( 'NONE',  ( -1.600000000000004086, 0.000000000000000000, -6.735000000000022524 ) ) ;
#10854=VERTEX_POINT ( 'NONE', #21643 ) ;
#10855=FACE_OUTER_BOUND ( 'NONE', #20320, .T. ) ;
#10898=LINE ( 'NONE', #18064, #6109 ) ;
#10904=DIRECTION ( 'NONE',  ( 0.000000000000000000, 0.000000000000000000, -1.000000000000000000 ) ) ;
#10928=PLANE ( 'NONE',  #21384 ) ;
#10929=DIRECTION ( 'NONE',  ( 1.000000000000000000, 0.000000000000000000, 0.000000000000000000 ) ) ;
#10950=ORIENTED_EDGE ( 'NONE', *, *, #19086, .F. ) ;
#10967=DIRECTION ( 'NONE',  ( 0.000000000000000000, 0.000000000000000000, -1.000000000000000000 ) ) ;
#10976=DIRECTION ( 'NONE',  ( 0.000000000000000000, 1.000000000000000000, -1.224646799147353207E-16 ) ) ;
#11006=AXIS2_PLACEMENT_3D ( 'NONE', #6093, #4649, #8378 ) ;
#11013=EDGE_LOOP ( 'NONE', ( #8528, #14965, #6453, #6084 ) ) ;
#11022=CIRCLE ( 'NONE', #2579, 9.000000000000023093 ) ;
#11037=CIRCLE ( 'NONE', #11419, 8.265000000000021885 ) ;
#11060=ORIENTED_EDGE ( 'NONE', *, *, #13054, .F. ) ;
#11084=ORIENTED_EDGE ( 'NONE', *, *, #23298, .F. ) ;
#11116=EDGE_LOOP ( 'NONE', ( #1538, #19253, #17279, #14840 ) ) ;
#11130=ORIENTED_EDGE ( 'NONE', *, *, #23395, .F. ) ;
#11157=CARTESIAN_POINT ( 'NONE',  ( -90.00000000000000000, 0.000000000000000000, 0.000000000000000000 ) ) ;
#11199=DIRECTION ( 'NONE',  ( 0.000000000000000000, 0.000000000000000000, -1.000000000000000000 ) ) ;
#11253=EDGE_CURVE ( 'NONE', #9804, #23245, #37, .T. ) ;
#11260=ORIENTED_EDGE ( 'NONE', *, *, #13054, .T. ) ;
#11261=CARTESIAN_POINT ( 'NONE',  ( 1.799999999999996048, 0.000000000000000000, -9.000000000000023093 ) ) ;
#11278=FACE_OUTER_BOUND ( 'NONE', #1488, .T. ) ;
#11295=DIRECTION ( 'NONE',  ( 1.000000000000000000, 0.000000000000000000, 0.000000000000000000 ) ) ;
#11296=EDGE_CURVE ( 'NONE', #12123, #4946, #1554, .T. ) ;
#11305=CARTESIAN_POINT ( 'NONE',  ( -90.00000000000000000, 0.000000000000000000, 0.000000000000000000 ) ) ;
#11313=CIRCLE ( 'NONE', #16656, 6.735000000000022524 ) ;
#11330=DIRECTION ( 'NONE',  ( 0.9021819276640002938, 5.282584191382323161E-17, 0.4313557341643536880 ) ) ;
#11342=AXIS2_PLACEMENT_3D ( 'NONE', #19013, #11633, #9822 ) ;
#11354=FACE_OUTER_BOUND ( 'NONE', #12214, .T. ) ;
#11390=FACE_OUTER_BOUND ( 'NONE', #13248, .T. ) ;
#11419=AXIS2_PLACEMENT_3D ( 'NONE', #2737, #11993, #17486 ) ;
#11443=AXIS2_PLACEMENT_3D ( 'NONE', #20980, #19549, #3264 ) ;
#11471=DIRECTION ( 'NONE',  ( 1.000000000000000000, 0.000000000000000000, 0.000000000000000000 ) ) ;
#11511=DIRECTION ( 'NONE',  ( 0.000000000000000000, 0.000000000000000000, -1.000000000000000000 ) ) ;
#11523=DIRECTION ( 'NONE',  ( 0.000000000000000000, 0.000000000000000000, -1.000000000000000000 ) ) ;
#11527=DIRECTION ( 'NONE',  ( 0.000000000000000000, 0.000000000000000000, -1.000000000000000000 ) ) ;
#11595=AXIS2_PLACEMENT_3D ( 'NONE', #5229, #7043, #6573 ) ;
#11633=DIRECTION ( 'NONE',  ( 0.000000000000000000, -1.000000000000000000, 0.000000000000000000 ) ) ;
#11636=ORIENTED_EDGE ( 'NONE', *, *, #14377, .T. ) ;
#11648=CYLINDRICAL_SURFACE ( 'NONE', #18688, 8.073750000000021743 ) ;
#11649=DIRECTION ( 'NONE',  ( 0.000000000000000000, 0.000000000000000000, -1.000000000000000000 ) ) ;
#11667=DIRECTION ( 'NONE',  ( 0.000000000000000000, 1.000000000000000000, -1.224646799147353207E-16 ) ) ;
#11678=CARTESIAN_POINT ( 'NONE',  ( -1.506022603841296270, 0.000000000000000000, 0.000000000000000000 ) ) ;
#11687=( LENGTH_UNIT ( ) NAMED_UNIT ( * ) SI_UNIT ( .MILLI., .METRE. ) );
#11714=ORIENTED_EDGE ( 'NONE', *, *, #12732, .T. ) ;
#11718=EDGE_LOOP ( 'NONE', ( #2815, #3350, #1861, #20151 ) ) ;
#11739=CARTESIAN_POINT ( 'NONE',  ( 1.519999999999999574, 8.279592079675421725E-16, 6.760799999999997034 ) ) ;
#11743=CARTESIAN_POINT ( 'NONE',  ( 1.506022603841296714, 8.263794135966437014E-16, 6.735000000000022524 ) ) ;
#11750=EDGE_LOOP ( 'NONE', ( #10950, #12979, #23194, #9430 ) ) ;
#11810=DIRECTION ( 'NONE',  ( 0.000000000000000000, 0.000000000000000000, -1.000000000000000000 ) ) ;
#11830=EDGE_CURVE ( 'NONE', #17305, #10717, #13081, .T. ) ;
#11861=DIRECTION ( 'NONE',  ( 1.000000000000000000, 0.000000000000000000, 0.000000000000000000 ) ) ;
#11862=AXIS2_PLACEMENT_3D ( 'NONE', #23597, #3358, #14641 ) ;
#11881=VERTEX_POINT ( 'NONE', #16518 ) ;
#11905=ADVANCED_FACE ( 'NONE', ( #9939 ), #7672, .T. ) ;
#11918=DIRECTION ( 'NONE',  ( 1.000000000000000000, 0.000000000000000000, 0.000000000000000000 ) ) ;
#11924=EDGE_LOOP ( 'NONE', ( #14014, #7674, #17036, #15140 ) ) ;
#11934=DIRECTION ( 'NONE',  ( 1.000000000000000000, 0.000000000000000000, 0.000000000000000000 ) ) ;
#11975=DIRECTION ( 'NONE',  ( 1.000000000000000000, 0.000000000000000000, 0.000000000000000000 ) ) ;
#11977=DIRECTION ( 'NONE',  ( 1.000000000000000000, 0.000000000000000000, 0.000000000000000000 ) ) ;
#11979=CARTESIAN_POINT ( 'NONE',  ( 2.000000000000001776, 0.000000000000000000, 0.000000000000000000 ) ) ;
#11993=DIRECTION ( 'NONE',  ( 1.000000000000000000, 0.000000000000000000, 0.000000000000000000 ) ) ;
#12003=VERTEX_POINT ( 'NONE', #566 ) ;
#12010=DIRECTION ( 'NONE',  ( 1.000000000000000000, 0.000000000000000000, 0.000000000000000000 ) ) ;
#12014=DIRECTION ( 'NONE',  ( 0.000000000000000000, 0.000000000000000000, -1.000000000000000000 ) ) ;
#12029=CARTESIAN_POINT ( 'NONE',  ( -1.506022603841296270, 0.000000000000000000, -6.735000000000022524 ) ) ;
#12074=ORIENTED_EDGE ( 'NONE', *, *, #9338, .F. ) ;
#12094=PLANE ( 'NONE',  #13503 ) ;
#12122=CARTESIAN_POINT ( 'NONE',  ( -1.799999999999996048, 7.470345474798879931E-16, 6.000000000000021316 ) ) ;
#12123=VERTEX_POINT ( 'NONE', #17929 ) ;
#12133=EDGE_CURVE ( 'NONE', #23443, #19414, #8447, .T. ) ;
#12143=CARTESIAN_POINT ( 'NONE',  ( -90.00000000000000000, 0.000000000000000000, -8.073750000000021743 ) ) ;
#12185=EDGE_CURVE ( 'NONE', #22332, #19003, #22165, .T. ) ;
#12189=CARTESIAN_POINT ( 'NONE',  ( -2.000000000000000888, 8.073750000000021743, 0.000000000000000000 ) ) ;
#12214=EDGE_LOOP ( 'NONE', ( #23107, #22591 ) ) ;
#12253=CARTESIAN_POINT ( 'NONE',  ( -90.00000000000000000, 9.887492094615969966E-16, 8.073750000000021743 ) ) ;
#12280=ORIENTED_EDGE ( 'NONE', *, *, #23535, .F. ) ;
#12308=ORIENTED_EDGE ( 'NONE', *, *, #7492, .T. ) ;
#12339=DIRECTION ( 'NONE',  ( 0.000000000000000000, 0.000000000000000000, -1.000000000000000000 ) ) ;
#12358=VERTEX_POINT ( 'NONE', #21004 ) ;
#12366=CYLINDRICAL_SURFACE ( 'NONE', #2081, 8.073750000000021743 ) ;
#12394=CARTESIAN_POINT ( 'NONE',  ( 2.000000000000001776, 0.000000000000000000, 0.000000000000000000 ) ) ;
#12396=CIRCLE ( 'NONE', #21134, 6.735000000000022524 ) ;
#12415=ORIENTED_EDGE ( 'NONE', *, *, #20746, .F. ) ;
#12427=ORIENTED_EDGE ( 'NONE', *, *, #14956, .T. ) ;
#12467=LINE ( 'NONE', #21878, #19097 ) ;
#12486=DIRECTION ( 'NONE',  ( 1.000000000000000000, -0.000000000000000000, -0.000000000000000000 ) ) ;
#12501=PRESENTATION_STYLE_ASSIGNMENT (( #7338 ) ) ;
#12557=AXIS2_PLACEMENT_3D ( 'NONE', #12189, #16006, #15891 ) ;
#12584=COLOUR_RGB ( '', 0.08235294, 0.09019608, 0.10196078) ;
#12592=CIRCLE ( 'NONE', #2951, 6.735000000000022524 ) ;
#12607=CARTESIAN_POINT ( 'NONE',  ( -90.00000000000000000, 0.000000000000000000, 0.000000000000000000 ) ) ;
#12617=DIRECTION ( 'NONE',  ( 0.000000000000000000, 0.000000000000000000, -1.000000000000000000 ) ) ;
#12621=AXIS2_PLACEMENT_3D ( 'NONE', #6588, #22984, #10321 ) ;
#12660=DIRECTION ( 'NONE',  ( -1.000000000000000000, -0.000000000000000000, -0.000000000000000000 ) ) ;
#12672=EDGE_LOOP ( 'NONE', ( #22367, #21008 ) ) ;
#12711=DIRECTION ( 'NONE',  ( 1.000000000000000000, 0.000000000000000000, 0.000000000000000000 ) ) ;
#12732=EDGE_CURVE ( 'NONE', #19018, #22332, #23341, .T. ) ;
#12736=CARTESIAN_POINT ( 'NONE',  ( -1.519999999999999796, 8.239200000000002078, 0.000000000000000000 ) ) ;
#12778=CIRCLE ( 'NONE', #13536, 8.073750000000021743 ) ;
#12805=DIRECTION ( 'NONE',  ( 1.000000000000000000, 0.000000000000000000, 0.000000000000000000 ) ) ;
#12844=ORIENTED_EDGE ( 'NONE', *, *, #9683, .F. ) ;
#12857=EDGE_LOOP ( 'NONE', ( #16538, #4024, #3584, #23497 ) ) ;
#12907=CARTESIAN_POINT ( 'NONE',  ( -1.800000000000000711, 7.592810154713614487E-16, 6.200000000000020606 ) ) ;
#12945=EDGE_CURVE ( 'NONE', #9531, #16003, #14588, .T. ) ;
#12947=ORIENTED_EDGE ( 'NONE', *, *, #19782, .F. ) ;
#12979=ORIENTED_EDGE ( 'NONE', *, *, #11253, .T. ) ;
#12986=ORIENTED_EDGE ( 'NONE', *, *, #7465, .T. ) ;
#13054=EDGE_CURVE ( 'NONE', #10661, #14897, #4611, .T. ) ;
#13081=CIRCLE ( 'NONE', #13798, 6.200000000000020606 ) ;
#13138=DIRECTION ( 'NONE',  ( 0.000000000000000000, 0.000000000000000000, -1.000000000000000000 ) ) ;
#13188=DIRECTION ( 'NONE',  ( 0.000000000000000000, 0.000000000000000000, -1.000000000000000000 ) ) ;
#13220=EDGE_CURVE ( 'NONE', #21260, #10183, #22833, .T. ) ;
#13248=EDGE_LOOP ( 'NONE', ( #11084, #15191, #16610, #5549 ) ) ;
#13258=TOROIDAL_SURFACE ( 'NONE', #2119, 6.760799999999997034, 0.03079999999999879709 ) ;
#13286=AXIS2_PLACEMENT_3D ( 'NONE', #5044, #19641, #17748 ) ;
#13300=FACE_OUTER_BOUND ( 'NONE', #8950, .T. ) ;
#13305=DIRECTION ( 'NONE',  ( 0.000000000000000000, 0.000000000000000000, -1.000000000000000000 ) ) ;
#13316=AXIS2_PLACEMENT_3D ( 'NONE', #14249, #10662, #21150 ) ;
#13326=DIRECTION ( 'NONE',  ( 0.000000000000000000, -1.000000000000000000, 0.000000000000000000 ) ) ;
#13375=DIRECTION ( 'NONE',  ( 0.000000000000000000, 0.000000000000000000, 1.000000000000000000 ) ) ;
#13399=AXIS2_PLACEMENT_3D ( 'NONE', #22623, #19026, #9606 ) ;
#13402=DIRECTION ( 'NONE',  ( 0.000000000000000000, 0.000000000000000000, -1.000000000000000000 ) ) ;
#13430=ORIENTED_EDGE ( 'NONE', *, *, #11296, .F. ) ;
#13461=DIRECTION ( 'NONE',  ( -0.9021819276639965191, 5.282584191382421768E-17, -0.4313557341643617371 ) ) ;
#13478=ORIENTED_EDGE ( 'NONE', *, *, #20892, .T. ) ;
#13499=CARTESIAN_POINT ( 'NONE',  ( -1.600000000000004086, 0.000000000000000000, -6.735000000000022524 ) ) ;
#13503=AXIS2_PLACEMENT_3D ( 'NONE', #19595, #8854, #19832 ) ;
#13516=CARTESIAN_POINT ( 'NONE',  ( -1.799999999999996048, 0.000000000000000000, 0.000000000000000000 ) ) ;
#13536=AXIS2_PLACEMENT_3D ( 'NONE', #22174, #5431, #18238 ) ;
#13537=ADVANCED_FACE ( 'NONE', ( #15871 ), #7556, .T. ) ;
#13538=DIRECTION ( 'NONE',  ( 1.000000000000000000, -0.000000000000000000, -0.000000000000000000 ) ) ;
#13562=PRODUCT ( 'radial cylindrical roller bearing_iso_ISO 15 RCR - 1712 - 24,SI,NC,24', 'radial cylindrical roller bearing_iso_ISO 15 RCR - 1712 - 24,SI,NC,24', '', ( #20484 ) ) ;
#13635=ADVANCED_FACE ( 'NONE', ( #11278 ), #15227, .T. ) ;
#13648=FACE_OUTER_BOUND ( 'NONE', #5970, .T. ) ;
#13713=ORIENTED_EDGE ( 'NONE', *, *, #14798, .T. ) ;
#13750=FACE_BOUND ( 'NONE', #19204, .T. ) ;
#13777=DIRECTION ( 'NONE',  ( 0.000000000000000000, 0.000000000000000000, -1.000000000000000000 ) ) ;
#13798=AXIS2_PLACEMENT_3D ( 'NONE', #2120, #9454, #22354 ) ;
#13804=LINE ( 'NONE', #19162, #5961 ) ;
#13841=CYLINDRICAL_SURFACE ( 'NONE', #14878, 8.265000000000021885 ) ;
#13872=PLANE ( 'NONE',  #6490 ) ;
#13877=EDGE_CURVE ( 'NONE', #16003, #9531, #11037, .T. ) ;
#13883=DIRECTION ( 'NONE',  ( 1.000000000000000000, 0.000000000000000000, 0.000000000000000000 ) ) ;
#13887=CARTESIAN_POINT ( 'NONE',  ( 2.000000000000001776, 0.000000000000000000, -8.800000000000023803 ) ) ;
#13892=DIRECTION ( 'NONE',  ( 0.000000000000000000, 1.224646799147333486E-16, 1.000000000000000000 ) ) ;
#13912=ORIENTED_EDGE ( 'NONE', *, *, #20892, .F. ) ;
#14014=ORIENTED_EDGE ( 'NONE', *, *, #6702, .F. ) ;
#14043=CIRCLE ( 'NONE', #13286, 6.200000000000021494 ) ;
#14073=AXIS2_PLACEMENT_3D ( 'NONE', #17773, #8807, #19788 ) ;
#14078=CIRCLE ( 'NONE', #8722, 8.073750000000021743 ) ;
#14092=ORIENTED_EDGE ( 'NONE', *, *, #12185, .F. ) ;
#14099=UNCERTAINTY_MEASURE_WITH_UNIT (LENGTH_MEASURE( 1.000000000000000082E-05 ), #7258, 'distance_accuracy_value', 'NONE');
#14155=CARTESIAN_POINT ( 'NONE',  ( 1.506022603841296714, 0.000000000000000000, 0.000000000000000000 ) ) ;
#14166=DIRECTION ( 'NONE',  ( 0.000000000000000000, 0.000000000000000000, -1.000000000000000000 ) ) ;
#14213=ORIENTED_EDGE ( 'NONE', *, *, #17260, .T. ) ;
#14215=( NAMED_UNIT ( * ) PLANE_ANGLE_UNIT ( ) SI_UNIT ( $, .RADIAN. ) );
#14217=EDGE_CURVE ( 'NONE', #19804, #23527, #8349, .T. ) ;
#14219=ORIENTED_EDGE ( 'NONE', *, *, #20777, .T. ) ;
#14237=FACE_OUTER_BOUND ( 'NONE', #11116, .T. ) ;
#14245=EDGE_CURVE ( 'NONE', #10661, #17331, #7207, .T. ) ;
#14249=CARTESIAN_POINT ( 'NONE',  ( -2.000000000000001776, 0.000000000000000000, 0.000000000000000000 ) ) ;
#14252=ORIENTED_EDGE ( 'NONE', *, *, #1901, .T. ) ;
#14274=PLANE ( 'NONE',  #7489 ) ;
#14277=VERTEX_POINT ( 'NONE', #8762 ) ;
#14334=PLANE ( 'NONE',  #12557 ) ;
#14357=DIRECTION ( 'NONE',  ( 0.000000000000000000, -1.000000000000000000, 0.000000000000000000 ) ) ;
#14371=EDGE_CURVE ( 'NONE', #10183, #21260, #7221, .T. ) ;
#14377=EDGE_CURVE ( 'NONE', #6003, #9988, #20943, .T. ) ;
#14389=DIRECTION ( 'NONE',  ( 0.000000000000000000, 0.000000000000000000, -1.000000000000000000 ) ) ;
#14450=ORIENTED_EDGE ( 'NONE', *, *, #7309, .T. ) ;
#14459=ORIENTED_EDGE ( 'NONE', *, *, #14371, .F. ) ;
#14470=DIRECTION ( 'NONE',  ( 0.000000000000000000, 1.224646799147353454E-16, 1.000000000000000000 ) ) ;
#14481=CIRCLE ( 'NONE', #4519, 8.073750000000021743 ) ;
#14504=EDGE_CURVE ( 'NONE', #10070, #11881, #18672, .T. ) ;
#14527=( LENGTH_UNIT ( ) NAMED_UNIT ( * ) SI_UNIT ( .MILLI., .METRE. ) );
#14571=CARTESIAN_POINT ( 'NONE',  ( -90.00000000000000000, 0.000000000000000000, -8.265000000000021885 ) ) ;
#14574=( NAMED_UNIT ( * ) SI_UNIT ( $, .STERADIAN. ) SOLID_ANGLE_UNIT ( ) );
#14588=CIRCLE ( 'NONE', #6910, 8.265000000000021885 ) ;
#14630=DIRECTION ( 'NONE',  ( 0.000000000000000000, 0.000000000000000000, -1.000000000000000000 ) ) ;
#14641=DIRECTION ( 'NONE',  ( 0.000000000000000000, 0.000000000000000000, -1.000000000000000000 ) ) ;
#14643=DIRECTION ( 'NONE',  ( 0.000000000000000000, 0.000000000000000000, -1.000000000000000000 ) ) ;
#14651=CARTESIAN_POINT ( 'NONE',  ( 2.000000000000001776, 0.000000000000000000, 0.000000000000000000 ) ) ;
#14689=AXIS2_PLACEMENT_3D ( 'NONE', #623, #11918, #19186 ) ;
#14746=CYLINDRICAL_SURFACE ( 'NONE', #20842, 8.073750000000021743 ) ;
#14766=MANIFOLD_SOLID_BREP ( 'InnerRace', #899 ) ;
#14793=DIRECTION ( 'NONE',  ( 0.000000000000000000, 0.000000000000000000, -1.000000000000000000 ) ) ;
#14798=EDGE_CURVE ( 'NONE', #14897, #10661, #21333, .T. ) ;
#14802=DIRECTION ( 'NONE',  ( 1.000000000000000000, 0.000000000000000000, 0.000000000000000000 ) ) ;
#14840=ORIENTED_EDGE ( 'NONE', *, *, #9071, .F. ) ;
#14878=AXIS2_PLACEMENT_3D ( 'NONE', #10016, #2785, #11810 ) ;
#14897=VERTEX_POINT ( 'NONE', #8737 ) ;
#14903=ORIENTED_EDGE ( 'NONE', *, *, #7309, .F. ) ;
#14945=EDGE_CURVE ( 'NONE', #16266, #2194, #19449, .T. ) ;
#14956=EDGE_CURVE ( 'NONE', #22848, #4946, #22888, .T. ) ;
#14965=ORIENTED_EDGE ( 'NONE', *, *, #20746, .T. ) ;
#14977=EDGE_LOOP ( 'NONE', ( #12280, #18761, #3417, #15857 ) ) ;
#14999=CARTESIAN_POINT ( 'NONE',  ( -90.00000000000000000, 0.000000000000000000, 0.000000000000000000 ) ) ;
#15001=DIRECTION ( 'NONE',  ( 1.000000000000000000, -0.000000000000000000, -0.000000000000000000 ) ) ;
#15021=EDGE_LOOP ( 'NONE', ( #15070, #2076 ) ) ;
#15054=CARTESIAN_POINT ( 'NONE',  ( 2.000000000000001776, 0.000000000000000000, 0.000000000000000000 ) ) ;
#15070=ORIENTED_EDGE ( 'NONE', *, *, #12133, .F. ) ;
#15078=EDGE_CURVE ( 'NONE', #23515, #701, #1849, .T. ) ;
#15105=DIRECTION ( 'NONE',  ( 0.000000000000000000, 0.000000000000000000, -1.000000000000000000 ) ) ;
#15110=ORIENTED_EDGE ( 'NONE', *, *, #11830, .F. ) ;
#15114=EDGE_CURVE ( 'NONE', #10854, #17331, #21730, .T. ) ;
#15133=VERTEX_POINT ( 'NONE', #8457 ) ;
#15140=ORIENTED_EDGE ( 'NONE', *, *, #14377, .F. ) ;
#15150=CARTESIAN_POINT ( 'NONE',  ( 1.520000000000000462, 0.000000000000000000, -8.239200000000002078 ) ) ;
#15185=FACE_BOUND ( 'NONE', #18024, .T. ) ;
#15191=ORIENTED_EDGE ( 'NONE', *, *, #14217, .F. ) ;
#15199=ORIENTED_EDGE ( 'NONE', *, *, #12185, .T. ) ;
#15227=TOROIDAL_SURFACE ( 'NONE', #1398, 6.200000000000020606, 0.1999999999999997613 ) ;
#15258=VECTOR ( 'NONE', #3141, 1000.000000000000000 ) ;
#15312=AXIS2_PLACEMENT_3D ( 'NONE', #18391, #5578, #1971 ) ;
#15364=DIRECTION ( 'NONE',  ( 1.000000000000000000, 0.000000000000000000, 0.000000000000000000 ) ) ;
#15378=LINE ( 'NONE', #2407, #8275 ) ;
#15397=ORIENTED_EDGE ( 'NONE', *, *, #12133, .T. ) ;
#15407=ADVANCED_FACE ( 'NONE', ( #20586 ), #11648, .F. ) ;
#15409=EDGE_LOOP ( 'NONE', ( #12415, #14459, #987, #12844 ) ) ;
#15423=TOROIDAL_SURFACE ( 'NONE', #1987, 8.800000000000022027, 0.2000000000000011768 ) ;
#15430=CARTESIAN_POINT ( 'NONE',  ( 1.489200000000000079, 0.000000000000000000, -8.239200000000002078 ) ) ;
#15470=CIRCLE ( 'NONE', #10498, 0.03079999999999923077 ) ;
#15519=CARTESIAN_POINT ( 'NONE',  ( -1.600000000000004086, 0.000000000000000000, 0.000000000000000000 ) ) ;
#15549=ORIENTED_EDGE ( 'NONE', *, *, #12945, .F. ) ;
#15573=ADVANCED_FACE ( 'NONE', ( #21162 ), #22908, .T. ) ;
#15618=CYLINDRICAL_SURFACE ( 'NONE', #22050, 8.265000000000021885 ) ;
#15629=CIRCLE ( 'NONE', #3725, 8.073750000000021743 ) ;
#15630=ORIENTED_EDGE ( 'NONE', *, *, #21459, .T. ) ;
#15637=DIRECTION ( 'NONE',  ( 0.000000000000000000, 0.000000000000000000, -1.000000000000000000 ) ) ;
#15700=ORIENTED_EDGE ( 'NONE', *, *, #6365, .T. ) ;
#15710=EDGE_CURVE ( 'NONE', #6666, #23109, #6091, .T. ) ;
#15740=EDGE_CURVE ( 'NONE', #19075, #18380, #21751, .T. ) ;
#15818=EDGE_CURVE ( 'NONE', #23109, #2045, #12467, .T. ) ;
#15822=CARTESIAN_POINT ( 'NONE',  ( -2.000000000000000888, 7.592810154713614487E-16, 6.200000000000020606 ) ) ;
#15845=TOROIDAL_SURFACE ( 'NONE', #6653, 6.760799999999997034, 0.03079999999999879709 ) ;
#15857=ORIENTED_EDGE ( 'NONE', *, *, #2201, .T. ) ;
#15871=FACE_OUTER_BOUND ( 'NONE', #4625, .T. ) ;
#15882=CYLINDRICAL_SURFACE ( 'NONE', #23198, 9.000000000000021316 ) ;
#15890=ORIENTED_EDGE ( 'NONE', *, *, #4830, .F. ) ;
#15891=DIRECTION ( 'NONE',  ( -0.000000000000000000, 0.000000000000000000, 1.000000000000000000 ) ) ;
#15909=FACE_BOUND ( 'NONE', #9855, .T. ) ;
#15913=AXIS2_PLACEMENT_3D ( 'NONE', #22834, #17469, #2830 ) ;
#15914=CARTESIAN_POINT ( 'NONE',  ( 1.799999999999996048, 0.000000000000000000, 0.000000000000000000 ) ) ;
#15925=ORIENTED_EDGE ( 'NONE', *, *, #14945, .T. ) ;
#15962=CARTESIAN_POINT ( 'NONE',  ( -2.000000000000001776, 0.000000000000000000, -6.543750000000021494 ) ) ;
#15982=CARTESIAN_POINT ( 'NONE',  ( -1.600000000000004086, 0.000000000000000000, 0.000000000000000000 ) ) ;
#16003=VERTEX_POINT ( 'NONE', #7656 ) ;
#16005=AXIS2_PLACEMENT_3D ( 'NONE', #18235, #145, #14793 ) ;
#16006=DIRECTION ( 'NONE',  ( -1.000000000000000000, 0.000000000000000000, -0.000000000000000000 ) ) ;
#16069=EDGE_LOOP ( 'NONE', ( #16130, #1810, #7821, #13912 ) ) ;
#16075=SURFACE_STYLE_FILL_AREA ( #5630 ) ;
#16130=ORIENTED_EDGE ( 'NONE', *, *, #4470, .F. ) ;
#16148=PLANE ( 'NONE',  #7883 ) ;
#16173=DIRECTION ( 'NONE',  ( 0.000000000000000000, 0.000000000000000000, -1.000000000000000000 ) ) ;
#16177=EDGE_LOOP ( 'NONE', ( #7297, #21846, #14450, #20076 ) ) ;
#16187=CARTESIAN_POINT ( 'NONE',  ( -1.489200000000000079, 0.000000000000000000, -6.760799999999997034 ) ) ;
#16202=ORIENTED_EDGE ( 'NONE', *, *, #7038, .T. ) ;
#16213=DIRECTION ( 'NONE',  ( 0.000000000000000000, 0.000000000000000000, -1.000000000000000000 ) ) ;
#16266=VERTEX_POINT ( 'NONE', #1374 ) ;
#16268=CARTESIAN_POINT ( 'NONE',  ( 1.520000000000000462, 1.010590785124388747E-15, 8.239200000000002078 ) ) ;
#16275=CIRCLE ( 'NONE', #21209, 8.265000000000021885 ) ;
#16280=CARTESIAN_POINT ( 'NONE',  ( 1.799999999999996048, 0.000000000000000000, 0.000000000000000000 ) ) ;
#16294=VECTOR ( 'NONE', #11975, 1000.000000000000000 ) ;
#16300=DIRECTION ( 'NONE',  ( 0.000000000000000000, 0.000000000000000000, -1.000000000000000000 ) ) ;
#16402=ORIENTED_EDGE ( 'NONE', *, *, #1994, .T. ) ;
#16406=DIRECTION ( 'NONE',  ( 1.000000000000000000, 0.000000000000000000, 0.000000000000000000 ) ) ;
#16417=CARTESIAN_POINT ( 'NONE',  ( -1.600000000000004086, 0.000000000000000000, 0.000000000000000000 ) ) ;
#16465=DIRECTION ( 'NONE',  ( 0.000000000000000000, 0.000000000000000000, -1.000000000000000000 ) ) ;
#16468=FILL_AREA_STYLE_COLOUR ( '', #6450 ) ;
#16484=EDGE_CURVE ( 'NONE', #11881, #14277, #16597, .T. ) ;
#16508=ORIENTED_EDGE ( 'NONE', *, *, #846, .F. ) ;
#16518=CARTESIAN_POINT ( 'NONE',  ( 1.600000000000004086, 9.887492094615969966E-16, 8.073750000000021743 ) ) ;
#16534=DIRECTION ( 'NONE',  ( 1.000000000000000000, 0.000000000000000000, 0.000000000000000000 ) ) ;
#16538=ORIENTED_EDGE ( 'NONE', *, *, #20866, .F. ) ;
#16550=DIRECTION ( 'NONE',  ( 0.000000000000000000, 1.224646799147353207E-16, 1.000000000000000000 ) ) ;
#16555=ORIENTED_EDGE ( 'NONE', *, *, #3759, .T. ) ;
#16597=LINE ( 'NONE', #4010, #3424 ) ;
#16610=ORIENTED_EDGE ( 'NONE', *, *, #20166, .T. ) ;
#16634=CARTESIAN_POINT ( 'NONE',  ( -90.00000000000000000, 1.012170579495290078E-15, 8.265000000000021885 ) ) ;
#16636=FACE_OUTER_BOUND ( 'NONE', #2606, .T. ) ;
#16638=CYLINDRICAL_SURFACE ( 'NONE', #9331, 6.000000000000021316 ) ;
#16648=DIRECTION ( 'NONE',  ( 0.000000000000000000, 0.000000000000000000, -1.000000000000000000 ) ) ;
#16656=AXIS2_PLACEMENT_3D ( 'NONE', #8250, #17699, #22958 ) ;
#16738=EDGE_CURVE ( 'NONE', #23245, #23109, #20994, .T. ) ;
#16766=AXIS2_PLACEMENT_3D ( 'NONE', #5863, #17006, #581 ) ;
#16808=TOROIDAL_SURFACE ( 'NONE', #15312, 6.760799999999997034, 0.03079999999999857851 ) ;
#16824=ORIENTED_EDGE ( 'NONE', *, *, #14217, .T. ) ;
#16831=FACE_OUTER_BOUND ( 'NONE', #17121, .T. ) ;
#16839=DIRECTION ( 'NONE',  ( -0.000000000000000000, -1.000000000000000000, -0.000000000000000000 ) ) ;
#16849=DIRECTION ( 'NONE',  ( 1.000000000000000000, 0.000000000000000000, 0.000000000000000000 ) ) ;
#16893=ORIENTED_EDGE ( 'NONE', *, *, #13877, .F. ) ;
#16909=EDGE_CURVE ( 'NONE', #2194, #3058, #4, .T. ) ;
#16948=EDGE_LOOP ( 'NONE', ( #1655, #14252 ) ) ;
#16993=EDGE_LOOP ( 'NONE', ( #12986, #15925, #2628, #23377 ) ) ;
#17006=DIRECTION ( 'NONE',  ( 1.000000000000000000, 0.000000000000000000, 0.000000000000000000 ) ) ;
#17036=ORIENTED_EDGE ( 'NONE', *, *, #5590, .T. ) ;
#17053=ORIENTED_EDGE ( 'NONE', *, *, #14504, .F. ) ;
#17121=EDGE_LOOP ( 'NONE', ( #7007, #18131, #6388, #9957 ) ) ;
#17153=DIRECTION ( 'NONE',  ( 0.000000000000000000, 1.224646799147333486E-16, 1.000000000000000000 ) ) ;
#17180=EDGE_CURVE ( 'NONE', #10717, #17305, #8244, .T. ) ;
#17242=DIRECTION ( 'NONE',  ( 1.000000000000000000, -0.000000000000000000, -0.000000000000000000 ) ) ;
#17260=EDGE_CURVE ( 'NONE', #14897, #10854, #19267, .T. ) ;
#17267=DIRECTION ( 'NONE',  ( 0.000000000000000000, 0.000000000000000000, -1.000000000000000000 ) ) ;
#17279=ORIENTED_EDGE ( 'NONE', *, *, #7397, .F. ) ;
#17305=VERTEX_POINT ( 'NONE', #15822 ) ;
#17331=VERTEX_POINT ( 'NONE', #3104 ) ;
#17349=ORIENTED_EDGE ( 'NONE', *, *, #17260, .F. ) ;
#17378=CARTESIAN_POINT ( 'NONE',  ( 1.799999999999996048, 0.000000000000000000, -6.000000000000022204 ) ) ;
#17419=TOROIDAL_SURFACE ( 'NONE', #7088, 8.800000000000023803, 0.2000000000000000944 ) ;
#17423=CYLINDRICAL_SURFACE ( 'NONE', #7225, 6.735000000000022524 ) ;
#17469=DIRECTION ( 'NONE',  ( 1.000000000000000000, 0.000000000000000000, 0.000000000000000000 ) ) ;
#17486=DIRECTION ( 'NONE',  ( 0.000000000000000000, 0.000000000000000000, -1.000000000000000000 ) ) ;
#17510=ORIENTED_EDGE ( 'NONE', *, *, #14245, .T. ) ;
#17529=AXIS2_PLACEMENT_3D ( 'NONE', #2072, #10976, #22190 ) ;
#17566=EDGE_LOOP ( 'NONE', ( #9658, #498, #16402, #22359 ) ) ;
#17593=CIRCLE ( 'NONE', #1886, 0.03079999999999836341 ) ;
#17618=ADVANCED_FACE ( 'NONE', ( #20557 ), #8012, .F. ) ;
#17650=AXIS2_PLACEMENT_3D ( 'NONE', #2473, #18999, #22828 ) ;
#17675=DIRECTION ( 'NONE',  ( 1.000000000000000000, 0.000000000000000000, 0.000000000000000000 ) ) ;
#17677=EDGE_LOOP ( 'NONE', ( #23669, #17053, #6708, #15700 ) ) ;
#17680=ORIENTED_EDGE ( 'NONE', *, *, #7397, .T. ) ;
#17699=DIRECTION ( 'NONE',  ( 1.000000000000000000, -0.000000000000000000, -0.000000000000000000 ) ) ;
#17717=EDGE_CURVE ( 'NONE', #15133, #2790, #11313, .T. ) ;
#17748=DIRECTION ( 'NONE',  ( 0.000000000000000000, 0.000000000000000000, -1.000000000000000000 ) ) ;
#17773=CARTESIAN_POINT ( 'NONE',  ( -1.489200000000000301, 0.000000000000000000, 0.000000000000000000 ) ) ;
#17782=DIRECTION ( 'NONE',  ( 0.000000000000000000, 0.000000000000000000, 1.000000000000000000 ) ) ;
#17843=DIRECTION ( 'NONE',  ( 1.000000000000000000, 0.000000000000000000, 0.000000000000000000 ) ) ;
#17855=DIRECTION ( 'NONE',  ( 1.000000000000000000, 0.000000000000000000, 0.000000000000000000 ) ) ;
#17864=AXIS2_PLACEMENT_3D ( 'NONE', #20383, #20139, #10967 ) ;
#17872=ORIENTED_EDGE ( 'NONE', *, *, #2671, .T. ) ;
#17875=EDGE_LOOP ( 'NONE', ( #21161, #3259, #3421, #1416 ) ) ;
#17888=DIRECTION ( 'NONE',  ( 1.000000000000000000, 0.000000000000000000, 0.000000000000000000 ) ) ;
#17929=CARTESIAN_POINT ( 'NONE',  ( 2.000000000000000000, 0.000000000000000000, -6.200000000000021494 ) ) ;
#17956=AXIS2_PLACEMENT_3D ( 'NONE', #8872, #3568, #10904 ) ;
#17962=ORIENTED_EDGE ( 'NONE', *, *, #8261, .F. ) ;
#17968=CARTESIAN_POINT ( 'NONE',  ( 1.489200000000000079, 0.000000000000000000, 0.000000000000000000 ) ) ;
#17979=EDGE_CURVE ( 'NONE', #23527, #17305, #6711, .T. ) ;
#17981=AXIS2_PLACEMENT_3D ( 'NONE', #8602, #14357, #21501 ) ;
#18000=AXIS2_PLACEMENT_3D ( 'NONE', #3829, #7797, #16648 ) ;
#18024=EDGE_LOOP ( 'NONE', ( #1453, #3551 ) ) ;
#18026=FILL_AREA_STYLE ('',( #16468 ) ) ;
#18064=CARTESIAN_POINT ( 'NONE',  ( 2.000000000000001776, 0.000000000000000000, 6.543750000000017053 ) ) ;
#18076=DIRECTION ( 'NONE',  ( 1.000000000000000000, -0.000000000000000000, -0.000000000000000000 ) ) ;
#18081=CARTESIAN_POINT ( 'NONE',  ( -1.799999999999996048, 0.000000000000000000, -6.000000000000021316 ) ) ;
#18090=DIRECTION ( 'NONE',  ( 0.000000000000000000, 0.000000000000000000, 1.000000000000000000 ) ) ;
#18097=CARTESIAN_POINT ( 'NONE',  ( 2.000000000000000000, 7.592810154713616459E-16, 6.200000000000021494 ) ) ;
#18131=ORIENTED_EDGE ( 'NONE', *, *, #20866, .T. ) ;
#18173=EDGE_LOOP ( 'NONE', ( #21683, #17872, #9152, #209 ) ) ;
#18189=CIRCLE ( 'NONE', #7876, 0.03079999999999923077 ) ;
#18213=CARTESIAN_POINT ( 'NONE',  ( -90.00000000000000000, 0.000000000000000000, -8.265000000000021885 ) ) ;
#18231=EDGE_CURVE ( 'NONE', #15133, #2520, #9936, .T. ) ;
#18235=CARTESIAN_POINT ( 'NONE',  ( -1.799999999999996048, 0.000000000000000000, 0.000000000000000000 ) ) ;
#18238=DIRECTION ( 'NONE',  ( 0.000000000000000000, 0.000000000000000000, -1.000000000000000000 ) ) ;
#18257=ADVANCED_FACE ( 'NONE', ( #4520 ), #8651, .T. ) ;
#18290=EDGE_CURVE ( 'NONE', #5128, #19003, #22381, .T. ) ;
#18302=STYLED_ITEM ( 'NONE', ( #7961 ), #23316 ) ;
#18321=CARTESIAN_POINT ( 'NONE',  ( 1.520000000000000462, 0.000000000000000000, 0.000000000000000000 ) ) ;
#18352=ORIENTED_EDGE ( 'NONE', *, *, #20777, .F. ) ;
#18368=AXIS2_PLACEMENT_3D ( 'NONE', #6330, #11977, #1036 ) ;
#18380=VERTEX_POINT ( 'NONE', #11739 ) ;
#18387=DIRECTION ( 'NONE',  ( 1.000000000000000000, 0.000000000000000000, 0.000000000000000000 ) ) ;
#18391=CARTESIAN_POINT ( 'NONE',  ( -1.489200000000000079, 0.000000000000000000, 0.000000000000000000 ) ) ;
#18408=EDGE_LOOP ( 'NONE', ( #539, #6548, #1276, #19363 ) ) ;
#18440=FACE_BOUND ( 'NONE', #8998, .T. ) ;
#18454=CARTESIAN_POINT ( 'NONE',  ( 2.000000000000001776, 0.000000000000000000, 6.543750000000017053 ) ) ;
#18579=DIRECTION ( 'NONE',  ( 1.000000000000000000, 0.000000000000000000, 0.000000000000000000 ) ) ;
#18629=ORIENTED_EDGE ( 'NONE', *, *, #21797, .F. ) ;
#18656=AXIS2_PLACEMENT_3D ( 'NONE', #10402, #410, #20035 ) ;
#18663=ADVANCED_FACE ( 'NONE', ( #11354, #15185 ), #7863, .T. ) ;
#18667=DIRECTION ( 'NONE',  ( 0.000000000000000000, 0.000000000000000000, -1.000000000000000000 ) ) ;
#18668=DIRECTION ( 'NONE',  ( 1.000000000000000000, 0.000000000000000000, 0.000000000000000000 ) ) ;
#18672=CIRCLE ( 'NONE', #16766, 8.073750000000021743 ) ;
#18683=DIRECTION ( 'NONE',  ( 1.000000000000000000, 0.000000000000000000, 0.000000000000000000 ) ) ;
#18688=AXIS2_PLACEMENT_3D ( 'NONE', #358, #18683, #7691 ) ;
#18747=DIRECTION ( 'NONE',  ( 0.000000000000000000, 0.000000000000000000, -1.000000000000000000 ) ) ;
#18761=ORIENTED_EDGE ( 'NONE', *, *, #15710, .T. ) ;
#18814=LINE ( 'NONE', #3714, #6912 ) ;
#18925=CARTESIAN_POINT ( 'NONE',  ( -90.00000000000000000, 0.000000000000000000, 0.000000000000000000 ) ) ;
#18936=LINE ( 'NONE', #4681, #7110 ) ;
#18999=DIRECTION ( 'NONE',  ( 1.000000000000000000, 0.000000000000000000, 0.000000000000000000 ) ) ;
#19003=VERTEX_POINT ( 'NONE', #3160 ) ;
#19013=CARTESIAN_POINT ( 'NONE',  ( -1.800000000000000711, 0.000000000000000000, -6.200000000000020606 ) ) ;
#19015=CARTESIAN_POINT ( 'NONE',  ( -1.520000000000000462, 0.000000000000000000, 0.000000000000000000 ) ) ;
#19018=VERTEX_POINT ( 'NONE', #21351 ) ;
#19026=DIRECTION ( 'NONE',  ( 1.000000000000000000, 0.000000000000000000, 0.000000000000000000 ) ) ;
#19055=( GEOMETRIC_REPRESENTATION_CONTEXT ( 3 ) GLOBAL_UNCERTAINTY_ASSIGNED_CONTEXT ( ( #9798 ) ) GLOBAL_UNIT_ASSIGNED_CONTEXT ( ( #11687, #20744, #22303 ) ) REPRESENTATION_CONTEXT ( 'NONE', 'WORKASPACE' ) );
#19075=VERTEX_POINT ( 'NONE', #401 ) ;
#19086=EDGE_CURVE ( 'NONE', #9804, #6666, #21942, .T. ) ;
#19097=VECTOR ( 'NONE', #23452, 1000.000000000000000 ) ;
#19115=AXIS2_PLACEMENT_3D ( 'NONE', #1877, #20073, #3673 ) ;
#19122=CIRCLE ( 'NONE', #4599, 0.2000000000000005107 ) ;
#19138=FACE_OUTER_BOUND ( 'NONE', #21640, .T. ) ;
#19155=FACE_OUTER_BOUND ( 'NONE', #23049, .T. ) ;
#19162=CARTESIAN_POINT ( 'NONE',  ( -90.00000000000000000, 8.247996192257451316E-16, 6.735000000000022524 ) ) ;
#19166=ADVANCED_FACE ( 'NONE', ( #5913 ), #5671, .T. ) ;
#19186=DIRECTION ( 'NONE',  ( 0.000000000000000000, 0.000000000000000000, -1.000000000000000000 ) ) ;
#19204=EDGE_LOOP ( 'NONE', ( #816, #16508 ) ) ;
#19247=CIRCLE ( 'NONE', #22298, 6.735000000000022524 ) ;
#19253=ORIENTED_EDGE ( 'NONE', *, *, #4470, .T. ) ;
#19267=LINE ( 'NONE', #1289, #6320 ) ;
#19283=EDGE_LOOP ( 'NONE', ( #19520, #19678 ) ) ;
#19291=CARTESIAN_POINT ( 'NONE',  ( -1.600000000000004086, 0.000000000000000000, -8.265000000000021885 ) ) ;
#19296=DIRECTION ( 'NONE',  ( 0.000000000000000000, 1.000000000000000000, -1.224646799147353207E-16 ) ) ;
#19363=ORIENTED_EDGE ( 'NONE', *, *, #7038, .F. ) ;
#19373=ORIENTED_EDGE ( 'NONE', *, *, #18231, .T. ) ;
#19414=VERTEX_POINT ( 'NONE', #3011 ) ;
#19429=MECHANICAL_DESIGN_GEOMETRIC_PRESENTATION_REPRESENTATION('',(#2212),#22489);
#19441=DIRECTION ( 'NONE',  ( 0.9021819276640002938, 0.000000000000000000, -0.4313557341643536880 ) ) ;
#19449=CIRCLE ( 'NONE', #20958, 0.2000000000000005107 ) ;
#19461=FACE_OUTER_BOUND ( 'NONE', #8548, .T. ) ;
#19520=ORIENTED_EDGE ( 'NONE', *, *, #1393, .F. ) ;
#19535=DIRECTION ( 'NONE',  ( 1.000000000000000000, 0.000000000000000000, 0.000000000000000000 ) ) ;
#19549=DIRECTION ( 'NONE',  ( 1.000000000000000000, 0.000000000000000000, 0.000000000000000000 ) ) ;
#19570=CARTESIAN_POINT ( 'NONE',  ( 1.489200000000000079, 0.000000000000000000, 0.000000000000000000 ) ) ;
#19579=ADVANCED_FACE ( 'NONE', ( #19745, #1190 ), #14274, .T. ) ;
#19595=CARTESIAN_POINT ( 'NONE',  ( -1.600000000000000977, 8.265000000000021885, 0.000000000000000000 ) ) ;
#19611=VERTEX_POINT ( 'NONE', #23103 ) ;
#19621=AXIS2_PLACEMENT_3D ( 'NONE', #11678, #22541, #22413 ) ;
#19623=CARTESIAN_POINT ( 'NONE',  ( 1.600000000000004086, 0.000000000000000000, -6.735000000000022524 ) ) ;
#19625=ORIENTED_EDGE ( 'NONE', *, *, #11830, .T. ) ;
#19641=DIRECTION ( 'NONE',  ( 1.000000000000000000, 0.000000000000000000, 0.000000000000000000 ) ) ;
#19651=EDGE_LOOP ( 'NONE', ( #10508, #1408, #14213, #8420 ) ) ;
#19659=DIRECTION ( 'NONE',  ( 0.000000000000000000, 0.000000000000000000, -1.000000000000000000 ) ) ;
#19678=ORIENTED_EDGE ( 'NONE', *, *, #12732, .F. ) ;
#19686=DIRECTION ( 'NONE',  ( 1.000000000000000000, 0.000000000000000000, 0.000000000000000000 ) ) ;
#19696=VECTOR ( 'NONE', #19686, 1000.000000000000000 ) ;
#19716=CIRCLE ( 'NONE', #22781, 6.760799999999997034 ) ;
#19722=DIRECTION ( 'NONE',  ( 1.000000000000000000, -0.000000000000000000, -0.000000000000000000 ) ) ;
#19729=ORIENTED_EDGE ( 'NONE', *, *, #2671, .F. ) ;
#19745=FACE_OUTER_BOUND ( 'NONE', #23615, .T. ) ;
#19754=EDGE_LOOP ( 'NONE', ( #7406, #3199 ) ) ;
#19766=ADVANCED_FACE ( 'NONE', ( #16636 ), #14746, .F. ) ;
#19782=EDGE_CURVE ( 'NONE', #701, #23515, #16275, .T. ) ;
#19788=DIRECTION ( 'NONE',  ( 0.000000000000000000, 0.000000000000000000, -1.000000000000000000 ) ) ;
#19804=VERTEX_POINT ( 'NONE', #18081 ) ;
#19812=FACE_OUTER_BOUND ( 'NONE', #19283, .T. ) ;
#19822=AXIS2_PLACEMENT_3D ( 'NONE', #15982, #17888, #10616 ) ;
#19832=DIRECTION ( 'NONE',  ( 0.000000000000000000, 0.000000000000000000, -1.000000000000000000 ) ) ;
#19877=AXIS2_PLACEMENT_3D ( 'NONE', #14651, #12, #23606 ) ;
#19881=DIRECTION ( 'NONE',  ( 0.000000000000000000, 0.000000000000000000, -1.000000000000000000 ) ) ;
#19963=DIRECTION ( 'NONE',  ( 0.000000000000000000, 0.000000000000000000, -1.000000000000000000 ) ) ;
#19992=DIRECTION ( 'NONE',  ( 0.000000000000000000, 1.224646799147353454E-16, 1.000000000000000000 ) ) ;
#20035=DIRECTION ( 'NONE',  ( -0.000000000000000000, 0.000000000000000000, 1.000000000000000000 ) ) ;
#20073=DIRECTION ( 'NONE',  ( -1.000000000000000000, 0.000000000000000000, 0.000000000000000000 ) ) ;
#20076=ORIENTED_EDGE ( 'NONE', *, *, #4361, .F. ) ;
#20078=DIRECTION ( 'NONE',  ( 1.000000000000000000, -0.000000000000000000, -0.000000000000000000 ) ) ;
#20092=DIRECTION ( 'NONE',  ( 0.000000000000000000, 0.000000000000000000, -1.000000000000000000 ) ) ;
#20125=ADVANCED_FACE ( 'NONE', ( #9059 ), #10550, .T. ) ;
#20129=CARTESIAN_POINT ( 'NONE',  ( 1.600000000000004086, 0.000000000000000000, -8.073750000000021743 ) ) ;
#20135=CYLINDRICAL_SURFACE ( 'NONE', #364, 6.735000000000022524 ) ;
#20136=CIRCLE ( 'NONE', #7995, 6.735000000000022524 ) ;
#20137=TOROIDAL_SURFACE ( 'NONE', #6414, 6.760799999999997034, 0.03079999999999857851 ) ;
#20139=DIRECTION ( 'NONE',  ( -1.000000000000000000, 0.000000000000000000, 0.000000000000000000 ) ) ;
#20151=ORIENTED_EDGE ( 'NONE', *, *, #18231, .F. ) ;
#20166=EDGE_CURVE ( 'NONE', #19804, #4946, #23524, .T. ) ;
#20170=VECTOR ( 'NONE', #3232, 1000.000000000000000 ) ;
#20188=DIRECTION ( 'NONE',  ( -0.9021819276639965191, 0.000000000000000000, 0.4313557341643617371 ) ) ;
#20210=AXIS2_PLACEMENT_3D ( 'NONE', #643, #6048, #13375 ) ;
#20228=DIRECTION ( 'NONE',  ( 1.000000000000000000, 0.000000000000000000, 0.000000000000000000 ) ) ;
#20249=ORIENTED_EDGE ( 'NONE', *, *, #8079, .F. ) ;
#20320=EDGE_LOOP ( 'NONE', ( #23612, #6609, #16202, #12074 ) ) ;
#20324=LINE ( 'NONE', #16634, #2429 ) ;
#20326=DIRECTION ( 'NONE',  ( 1.000000000000000000, -0.000000000000000000, -0.000000000000000000 ) ) ;
#20360=FACE_OUTER_BOUND ( 'NONE', #18408, .T. ) ;
#20383=CARTESIAN_POINT ( 'NONE',  ( -1.506022603841227436, 0.000000000000000000, 0.000000000000000000 ) ) ;
#20392=DIRECTION ( 'NONE',  ( 0.000000000000000000, 0.000000000000000000, -1.000000000000000000 ) ) ;
#20393=CARTESIAN_POINT ( 'NONE',  ( 1.489200000000000079, 0.000000000000000000, -6.760799999999997034 ) ) ;
#20444=CIRCLE ( 'NONE', #4009, 6.200000000000021494 ) ;
#20453=DIRECTION ( 'NONE',  ( 1.000000000000000000, 0.000000000000000000, 0.000000000000000000 ) ) ;
#20484=PRODUCT_CONTEXT ( 'NONE', #4859, 'mechanical' ) ;
#20506=CARTESIAN_POINT ( 'NONE',  ( -90.00000000000000000, 0.000000000000000000, 0.000000000000000000 ) ) ;
#20514=DIRECTION ( 'NONE',  ( -1.000000000000000000, -0.000000000000000000, -0.000000000000000000 ) ) ;
#20531=CARTESIAN_POINT ( 'NONE',  ( 1.999999999999998668, 6.200000000000021494, 0.000000000000000000 ) ) ;
#20546=AXIS2_PLACEMENT_3D ( 'NONE', #8858, #3443, #13892 ) ;
#20557=FACE_OUTER_BOUND ( 'NONE', #6935, .T. ) ;
#20586=FACE_OUTER_BOUND ( 'NONE', #17677, .T. ) ;
#20624=FACE_OUTER_BOUND ( 'NONE', #11718, .T. ) ;
#20645=ADVANCED_FACE ( 'NONE', ( #20360 ), #3970, .T. ) ;
#20665=DIRECTION ( 'NONE',  ( 1.000000000000000000, 0.000000000000000000, 0.000000000000000000 ) ) ;
#20679=CARTESIAN_POINT ( 'NONE',  ( 1.799999999999999156, 0.000000000000000000, -6.200000000000021494 ) ) ;
#20706=DIRECTION ( 'NONE',  ( 1.000000000000000000, 0.000000000000000000, 0.000000000000000000 ) ) ;
#20744=( NAMED_UNIT ( * ) PLANE_ANGLE_UNIT ( ) SI_UNIT ( $, .RADIAN. ) );
#20746=EDGE_CURVE ( 'NONE', #21260, #7327, #18936, .T. ) ;
#20760=AXIS2_PLACEMENT_3D ( 'NONE', #3341, #18076, #16173 ) ;
#20776=ORIENTED_EDGE ( 'NONE', *, *, #17717, .F. ) ;
#20777=EDGE_CURVE ( 'NONE', #18380, #2790, #18189, .T. ) ;
#20806=CARTESIAN_POINT ( 'NONE',  ( -1.506022603841227436, 1.012170579495290078E-15, 8.265000000000021885 ) ) ;
#20807=ORIENTED_EDGE ( 'NONE', *, *, #5590, .F. ) ;
#20822=CIRCLE ( 'NONE', #3241, 6.735000000000022524 ) ;
#20842=AXIS2_PLACEMENT_3D ( 'NONE', #12607, #217, #14630 ) ;
#20866=EDGE_CURVE ( 'NONE', #2595, #2520, #15378, .T. ) ;
#20892=EDGE_CURVE ( 'NONE', #8470, #12358, #19716, .T. ) ;
#20896=ADVANCED_FACE ( 'NONE', ( #2989 ), #13258, .T. ) ;
#20918=ORIENTED_EDGE ( 'NONE', *, *, #16909, .F. ) ;
#20932=CARTESIAN_POINT ( 'NONE',  ( -2.000000000000000888, 0.000000000000000000, -6.200000000000020606 ) ) ;
#20943=CIRCLE ( 'NONE', #1070, 8.239200000000002078 ) ;
#20958=AXIS2_PLACEMENT_3D ( 'NONE', #10791, #23450, #21758 ) ;
#20968=ORIENTED_EDGE ( 'NONE', *, *, #17979, .F. ) ;
#20980=CARTESIAN_POINT ( 'NONE',  ( 1.799999999999996048, 0.000000000000000000, 0.000000000000000000 ) ) ;
#20994=LINE ( 'NONE', #13499, #6136 ) ;
#21004=CARTESIAN_POINT ( 'NONE',  ( -1.519999999999999574, 0.000000000000000000, -6.760799999999997034 ) ) ;
#21006=AXIS2_PLACEMENT_3D ( 'NONE', #1476, #12660, #17782 ) ;
#21008=ORIENTED_EDGE ( 'NONE', *, *, #11253, .F. ) ;
#21038=ADVANCED_FACE ( 'NONE', ( #11390 ), #6485, .F. ) ;
#21045=CARTESIAN_POINT ( 'NONE',  ( 1.600000000000004086, 0.000000000000000000, -8.265000000000021885 ) ) ;
#21057=ORIENTED_EDGE ( 'NONE', *, *, #6365, .F. ) ;
#21134=AXIS2_PLACEMENT_3D ( 'NONE', #1706, #4969, #10623 ) ;
#21150=DIRECTION ( 'NONE',  ( 0.000000000000000000, 0.000000000000000000, -1.000000000000000000 ) ) ;
#21151=ORIENTED_EDGE ( 'NONE', *, *, #3484, .F. ) ;
#21161=ORIENTED_EDGE ( 'NONE', *, *, #7503, .T. ) ;
#21162=FACE_OUTER_BOUND ( 'NONE', #3790, .T. ) ;
#21169=EDGE_LOOP ( 'NONE', ( #6303, #10191, #2647, #14092 ) ) ;
#21209=AXIS2_PLACEMENT_3D ( 'NONE', #22005, #20326, #3470 ) ;
#21227=AXIS2_PLACEMENT_3D ( 'NONE', #20531, #16849, #22081 ) ;
#21239=ORIENTED_EDGE ( 'NONE', *, *, #6702, .T. ) ;
#21260=VERTEX_POINT ( 'NONE', #578 ) ;
#21277=AXIS2_PLACEMENT_3D ( 'NONE', #15430, #2567, #9675 ) ;
#21301=CIRCLE ( 'NONE', #7190, 6.760799999999997034 ) ;
#21302=DIRECTION ( 'NONE',  ( 1.000000000000000000, 0.000000000000000000, 0.000000000000000000 ) ) ;
#21317=CIRCLE ( 'NONE', #17529, 0.03079999999999923077 ) ;
#21333=CIRCLE ( 'NONE', #5283, 8.073750000000021743 ) ;
#21351=CARTESIAN_POINT ( 'NONE',  ( -2.000000000000001776, 1.089935651241147118E-15, 8.800000000000022027 ) ) ;
#21352=ORIENTED_EDGE ( 'NONE', *, *, #19782, .T. ) ;
#21382=DIRECTION ( 'NONE',  ( -1.000000000000000000, 0.000000000000000000, -0.000000000000000000 ) ) ;
#21384=AXIS2_PLACEMENT_3D ( 'NONE', #12736, #7214, #18090 ) ;
#21442=ORIENTED_EDGE ( 'NONE', *, *, #7492, .F. ) ;
#21459=EDGE_CURVE ( 'NONE', #19414, #23443, #5309, .T. ) ;
#21501=DIRECTION ( 'NONE',  ( 0.000000000000000000, 0.000000000000000000, -1.000000000000000000 ) ) ;
#21520=CARTESIAN_POINT ( 'NONE',  ( 1.520000000000000462, 0.000000000000000000, 0.000000000000000000 ) ) ;
#21544=CARTESIAN_POINT ( 'NONE',  ( -2.000000000000001776, 0.000000000000000000, 0.000000000000000000 ) ) ;
#21546=( NAMED_UNIT ( * ) PLANE_ANGLE_UNIT ( ) SI_UNIT ( $, .RADIAN. ) );
#21593=DIRECTION ( 'NONE',  ( 0.000000000000000000, 0.000000000000000000, -1.000000000000000000 ) ) ;
#21622=FACE_OUTER_BOUND ( 'NONE', #11750, .T. ) ;
#21640=EDGE_LOOP ( 'NONE', ( #21352, #21239, #8861, #20807 ) ) ;
#21643=CARTESIAN_POINT ( 'NONE',  ( -1.600000000000004086, 0.000000000000000000, -8.073750000000021743 ) ) ;
#21653=ORIENTED_EDGE ( 'NONE', *, *, #9683, .T. ) ;
#21657=SHAPE_REPRESENTATION ( 'radial cylindrical roller bearing_iso_ISO 15 RCR - 1712 - 24,SI,NC,24', ( #7318 ), #21725 ) ;
#21658=ADVANCED_FACE ( 'NONE', ( #9217 ), #4543, .T. ) ;
#21683=ORIENTED_EDGE ( 'NONE', *, *, #15078, .F. ) ;
#21692=FACE_OUTER_BOUND ( 'NONE', #16069, .T. ) ;
#21725=( GEOMETRIC_REPRESENTATION_CONTEXT ( 3 ) GLOBAL_UNCERTAINTY_ASSIGNED_CONTEXT ( ( #14099 ) ) GLOBAL_UNIT_ASSIGNED_CONTEXT ( ( #7258, #14215, #14574 ) ) REPRESENTATION_CONTEXT ( 'NONE', 'WORKASPACE' ) );
#21730=CIRCLE ( 'NONE', #19822, 8.073750000000021743 ) ;
#21751=CIRCLE ( 'NONE', #22140, 6.760799999999997034 ) ;
#21758=DIRECTION ( 'NONE',  ( 0.000000000000000000, 1.224646799147353207E-16, 1.000000000000000000 ) ) ;
#21797=EDGE_CURVE ( 'NONE', #23527, #19804, #4183, .T. ) ;
#21841=CARTESIAN_POINT ( 'NONE',  ( -90.00000000000000000, 0.000000000000000000, -6.000000000000021316 ) ) ;
#21846=ORIENTED_EDGE ( 'NONE', *, *, #16484, .T. ) ;
#21856=DIRECTION ( 'NONE',  ( 0.000000000000000000, 1.000000000000000000, -1.224646799147353207E-16 ) ) ;
#21878=CARTESIAN_POINT ( 'NONE',  ( -90.00000000000000000, 0.000000000000000000, -6.735000000000022524 ) ) ;
#21902=ADVANCED_FACE ( 'NONE', ( #6556, #13750 ), #13872, .T. ) ;
#21912=DIRECTION ( 'NONE',  ( 0.000000000000000000, 1.000000000000000000, -1.224646799147353207E-16 ) ) ;
#21942=LINE ( 'NONE', #22300, #23502 ) ;
#21947=EDGE_LOOP ( 'NONE', ( #21442, #15630, #412, #10556 ) ) ;
#21950=AXIS2_PLACEMENT_3D ( 'NONE', #8493, #13883, #6328 ) ;
#22005=CARTESIAN_POINT ( 'NONE',  ( 1.506022603841227436, 0.000000000000000000, 0.000000000000000000 ) ) ;
#22015=( NAMED_UNIT ( * ) SI_UNIT ( $, .STERADIAN. ) SOLID_ANGLE_UNIT ( ) );
#22039=CIRCLE ( 'NONE', #8320, 8.800000000000022027 ) ;
#22042=CARTESIAN_POINT ( 'NONE',  ( -1.799999999999996048, 0.000000000000000000, 0.000000000000000000 ) ) ;
#22050=AXIS2_PLACEMENT_3D ( 'NONE', #10223, #21302, #14166 ) ;
#22081=DIRECTION ( 'NONE',  ( 0.000000000000000000, 0.000000000000000000, -1.000000000000000000 ) ) ;
#22102=EDGE_LOOP ( 'NONE', ( #3291, #11636 ) ) ;
#22130=PRODUCT_DEFINITION_FORMATION_WITH_SPECIFIED_SOURCE ( 'ANY', '', #13562, .NOT_KNOWN. ) ;
#22140=AXIS2_PLACEMENT_3D ( 'NONE', #21520, #20078, #3805 ) ;
#22165=CIRCLE ( 'NONE', #17981, 0.2000000000000005107 ) ;
#22174=CARTESIAN_POINT ( 'NONE',  ( 1.600000000000004086, 0.000000000000000000, 0.000000000000000000 ) ) ;
#22181=LINE ( 'NONE', #14571, #4854 ) ;
#22190=DIRECTION ( 'NONE',  ( 0.000000000000000000, 1.224646799147333486E-16, 1.000000000000000000 ) ) ;
#22223=ADVANCED_FACE ( 'NONE', ( #14237 ), #16808, .T. ) ;
#22250=ORIENTED_EDGE ( 'NONE', *, *, #23298, .T. ) ;
#22298=AXIS2_PLACEMENT_3D ( 'NONE', #999, #11471, #18747 ) ;
#22300=CARTESIAN_POINT ( 'NONE',  ( -1.600000000000004086, 8.247996192257451316E-16, 6.735000000000022524 ) ) ;
#22303=( NAMED_UNIT ( * ) SI_UNIT ( $, .STERADIAN. ) SOLID_ANGLE_UNIT ( ) );
#22332=VERTEX_POINT ( 'NONE', #7154 ) ;
#22354=DIRECTION ( 'NONE',  ( 0.000000000000000000, 0.000000000000000000, -1.000000000000000000 ) ) ;
#22358=DIRECTION ( 'NONE',  ( 1.000000000000000000, 0.000000000000000000, 0.000000000000000000 ) ) ;
#22359=ORIENTED_EDGE ( 'NONE', *, *, #15818, .F. ) ;
#22362=FACE_OUTER_BOUND ( 'NONE', #16993, .T. ) ;
#22367=ORIENTED_EDGE ( 'NONE', *, *, #7503, .F. ) ;
#22381=CIRCLE ( 'NONE', #15913, 9.000000000000021316 ) ;
#22413=DIRECTION ( 'NONE',  ( 0.000000000000000000, 0.000000000000000000, -1.000000000000000000 ) ) ;
#22417=DIRECTION ( 'NONE',  ( 1.000000000000000000, 0.000000000000000000, 0.000000000000000000 ) ) ;
#22486=VERTEX_POINT ( 'NONE', #22687 ) ;
#22489=( GEOMETRIC_REPRESENTATION_CONTEXT ( 3 ) GLOBAL_UNCERTAINTY_ASSIGNED_CONTEXT ( ( #8588 ) ) GLOBAL_UNIT_ASSIGNED_CONTEXT ( ( #14527, #21546, #22015 ) ) REPRESENTATION_CONTEXT ( 'NONE', 'WORKASPACE' ) );
#22508=AXIS2_PLACEMENT_3D ( 'NONE', #16280, #12711, #19963 ) ;
#22520=SHAPE_DEFINITION_REPRESENTATION ( #3758, #21657 ) ;
#22541=DIRECTION ( 'NONE',  ( -1.000000000000000000, 0.000000000000000000, 0.000000000000000000 ) ) ;
#22546=CIRCLE ( 'NONE', #13399, 9.000000000000023093 ) ;
#22591=ORIENTED_EDGE ( 'NONE', *, *, #5834, .T. ) ;
#22594=VECTOR ( 'NONE', #10212, 1000.000000000000000 ) ;
#22623=CARTESIAN_POINT ( 'NONE',  ( 1.799999999999996048, 0.000000000000000000, 0.000000000000000000 ) ) ;
#22672=ADVANCED_FACE ( 'NONE', ( #10503 ), #2655, .T. ) ;
#22687=CARTESIAN_POINT ( 'NONE',  ( -1.506022603841227436, 0.000000000000000000, -8.265000000000021885 ) ) ;
#22697=ORIENTED_EDGE ( 'NONE', *, *, #8079, .T. ) ;
#22721=VECTOR ( 'NONE', #19535, 1000.000000000000000 ) ;
#22724=CARTESIAN_POINT ( 'NONE',  ( 1.489200000000000079, 0.000000000000000000, 0.000000000000000000 ) ) ;
#22732=ADVANCED_FACE ( 'NONE', ( #20624 ), #20135, .T. ) ;
#22781=AXIS2_PLACEMENT_3D ( 'NONE', #10457, #23221, #3351 ) ;
#22825=CIRCLE ( 'NONE', #17864, 8.265000000000021885 ) ;
#22828=DIRECTION ( 'NONE',  ( 0.000000000000000000, 0.000000000000000000, -1.000000000000000000 ) ) ;
#22833=CIRCLE ( 'NONE', #8323, 8.265000000000021885 ) ;
#22834=CARTESIAN_POINT ( 'NONE',  ( -1.799999999999996048, 0.000000000000000000, 0.000000000000000000 ) ) ;
#22848=VERTEX_POINT ( 'NONE', #3870 ) ;
#22870=DIRECTION ( 'NONE',  ( 0.000000000000000000, 0.000000000000000000, -1.000000000000000000 ) ) ;
#22878=CARTESIAN_POINT ( 'NONE',  ( 1.489200000000000079, 8.279592079675421725E-16, 6.760799999999997034 ) ) ;
#22888=CIRCLE ( 'NONE', #22508, 6.000000000000022204 ) ;
#22908=TOROIDAL_SURFACE ( 'NONE', #12621, 6.200000000000021494, 0.1999999999999996503 ) ;
#22934=ORIENTED_EDGE ( 'NONE', *, *, #484, .F. ) ;
#22958=DIRECTION ( 'NONE',  ( 0.000000000000000000, 0.000000000000000000, 1.000000000000000000 ) ) ;
#22984=DIRECTION ( 'NONE',  ( 1.000000000000000000, 0.000000000000000000, 0.000000000000000000 ) ) ;
#22994=CARTESIAN_POINT ( 'NONE',  ( -1.520000000000000462, 0.000000000000000000, -8.239200000000002078 ) ) ;
#23002=DIRECTION ( 'NONE',  ( 0.000000000000000000, 0.000000000000000000, -1.000000000000000000 ) ) ;
#23020=ORIENTED_EDGE ( 'NONE', *, *, #14945, .F. ) ;
#23049=EDGE_LOOP ( 'NONE', ( #23020, #4622, #8309, #20918 ) ) ;
#23052=EDGE_LOOP ( 'NONE', ( #15890, #1661, #19373, #22934 ) ) ;
#23103=CARTESIAN_POINT ( 'NONE',  ( -1.506022603841296270, 8.263794135966437014E-16, 6.735000000000022524 ) ) ;
#23107=ORIENTED_EDGE ( 'NONE', *, *, #2061, .T. ) ;
#23109=VERTEX_POINT ( 'NONE', #10829 ) ;
#23175=CARTESIAN_POINT ( 'NONE',  ( -1.600000000000004086, 0.000000000000000000, 0.000000000000000000 ) ) ;
#23186=FACE_OUTER_BOUND ( 'NONE', #12672, .T. ) ;
#23194=ORIENTED_EDGE ( 'NONE', *, *, #16738, .T. ) ;
#23198=AXIS2_PLACEMENT_3D ( 'NONE', #1479, #17675, #4845 ) ;
#23211=ORIENTED_EDGE ( 'NONE', *, *, #846, .T. ) ;
#23214=DIRECTION ( 'NONE',  ( 0.000000000000000000, 0.000000000000000000, -1.000000000000000000 ) ) ;
#23221=DIRECTION ( 'NONE',  ( 1.000000000000000000, -0.000000000000000000, -0.000000000000000000 ) ) ;
#23230=CIRCLE ( 'NONE', #20546, 0.03079999999999923077 ) ;
#23245=VERTEX_POINT ( 'NONE', #15962 ) ;
#23270=AXIS2_PLACEMENT_3D ( 'NONE', #14999, #20453, #13188 ) ;
#23278=CIRCLE ( 'NONE', #6089, 0.1999999999999996503 ) ;
#23298=EDGE_CURVE ( 'NONE', #23527, #22848, #18814, .T. ) ;
#23316=ADVANCED_BREP_SHAPE_REPRESENTATION ( '', ( #14766, #7318 ), #21725 ) ;
#23319=CIRCLE ( 'NONE', #19115, 8.265000000000021885 ) ;
#23336=AXIS2_PLACEMENT_3D ( 'NONE', #22042, #3864, #11199 ) ;
#23341=CIRCLE ( 'NONE', #3461, 8.800000000000022027 ) ;
#23377=ORIENTED_EDGE ( 'NONE', *, *, #2334, .F. ) ;
#23386=CARTESIAN_POINT ( 'NONE',  ( -1.519999999999999574, 8.279592079675421725E-16, 6.760799999999997034 ) ) ;
#23395=EDGE_CURVE ( 'NONE', #19018, #5128, #19122, .T. ) ;
#23443=VERTEX_POINT ( 'NONE', #22994 ) ;
#23450=DIRECTION ( 'NONE',  ( 0.000000000000000000, 1.000000000000000000, -1.224646799147353207E-16 ) ) ;
#23452=DIRECTION ( 'NONE',  ( 1.000000000000000000, 0.000000000000000000, 0.000000000000000000 ) ) ;
#23463=DIRECTION ( 'NONE',  ( 1.000000000000000000, 0.000000000000000000, 0.000000000000000000 ) ) ;
#23497=ORIENTED_EDGE ( 'NONE', *, *, #484, .T. ) ;
#23502=VECTOR ( 'NONE', #11330, 1000.000000000000114 ) ;
#23515=VERTEX_POINT ( 'NONE', #8409 ) ;
#23521=SURFACE_SIDE_STYLE ('',( #8942 ) ) ;
#23524=LINE ( 'NONE', #21841, #19696 ) ;
#23527=VERTEX_POINT ( 'NONE', #12122 ) ;
#23535=EDGE_CURVE ( 'NONE', #6666, #19611, #9730, .T. ) ;
#23572=ADVANCED_FACE ( 'NONE', ( #2751 ), #2513, .F. ) ;
#23597=CARTESIAN_POINT ( 'NONE',  ( 1.520000000000000462, 0.000000000000000000, 0.000000000000000000 ) ) ;
#23606=DIRECTION ( 'NONE',  ( 0.000000000000000000, 0.000000000000000000, -1.000000000000000000 ) ) ;
#23612=ORIENTED_EDGE ( 'NONE', *, *, #6031, .F. ) ;
#23615=EDGE_LOOP ( 'NONE', ( #2378, #8644 ) ) ;
#23669=ORIENTED_EDGE ( 'NONE', *, *, #16484, .F. ) ;
#23671=AXIS2_PLACEMENT_3D ( 'NONE', #5594, #1638, #3789 ) ;
#23697=DIRECTION ( 'NONE',  ( 1.000000000000000000, 0.000000000000000000, 0.000000000000000000 ) ) ;
ENDSEC;
END-ISO-10303-21;
